ISO-10303-21;
HEADER;
/* Generated by software containing ST-Developer
 * from STEP Tools, Inc. (www.steptools.com) 
 */

FILE_DESCRIPTION(
/* description */ ('Independent AHU equipment rack. Nominal800x600 frame on1000long40squa
re aluminum posts; two removable notched shelves; welded perimeter/cro
ss rails and rear gussets; two mounting channels; four isolation pads 
and anchor-ready feet. Imported native extrusion library retained and 
cut-length parameters customized per family. Shelf hardware uses model
ed M6 rivet nuts and screws. Weld design, floor anchors and load ratin
g require engineering selection.'),
/* implementation_level */ '2;1');

FILE_NAME(
/* name */ 'Socket head cap screw M6x12.step',
/* time_stamp */ '2026-11-07T19:04:45-08:00',
/* author */ (''),
/* organization */ (''),
/* preprocessor_version */ 'ST-DEVELOPER v20.2',
/* originating_system */ 'Autodesk Translation Framework v15.17.0.0',
/* authorisation */ '');

FILE_SCHEMA (('AUTOMOTIVE_DESIGN { 1 0 10303 214 3 1 1 }'));
ENDSEC;

DATA;
#10=MECHANICAL_DESIGN_GEOMETRIC_PRESENTATION_REPRESENTATION('',(#345),#9777);
#211=CONICAL_SURFACE('',#4283,2.5,0.785398163397449);
#214=B_SPLINE_SURFACE_WITH_KNOTS('',3,3,((#8793,#8794,#8795,#8796,#8797,
#8798,#8799,#8800,#8801,#8802,#8803,#8804,#8805,#8806,#8807,#8808,#8809,
#8810,#8811,#8812,#8813,#8814,#8815,#8816,#8817,#8818,#8819,#8820,#8821,
#8822,#8823,#8824,#8825,#8826,#8827,#8828,#8829,#8830,#8831,#8832,#8833,
#8834,#8835,#8836,#8837,#8838,#8839,#8840,#8841,#8842,#8843,#8844,#8845,
#8846,#8847,#8848,#8849,#8850,#8851,#8852,#8853,#8854,#8855,#8856,#8857,
#8858,#8859,#8860,#8861,#8862,#8863,#8864,#8865,#8866,#8867,#8868,#8869),
(#8870,#8871,#8872,#8873,#8874,#8875,#8876,#8877,#8878,#8879,#8880,#8881,
#8882,#8883,#8884,#8885,#8886,#8887,#8888,#8889,#8890,#8891,#8892,#8893,
#8894,#8895,#8896,#8897,#8898,#8899,#8900,#8901,#8902,#8903,#8904,#8905,
#8906,#8907,#8908,#8909,#8910,#8911,#8912,#8913,#8914,#8915,#8916,#8917,
#8918,#8919,#8920,#8921,#8922,#8923,#8924,#8925,#8926,#8927,#8928,#8929,
#8930,#8931,#8932,#8933,#8934,#8935,#8936,#8937,#8938,#8939,#8940,#8941,
#8942,#8943,#8944,#8945,#8946),(#8947,#8948,#8949,#8950,#8951,#8952,#8953,
#8954,#8955,#8956,#8957,#8958,#8959,#8960,#8961,#8962,#8963,#8964,#8965,
#8966,#8967,#8968,#8969,#8970,#8971,#8972,#8973,#8974,#8975,#8976,#8977,
#8978,#8979,#8980,#8981,#8982,#8983,#8984,#8985,#8986,#8987,#8988,#8989,
#8990,#8991,#8992,#8993,#8994,#8995,#8996,#8997,#8998,#8999,#9000,#9001,
#9002,#9003,#9004,#9005,#9006,#9007,#9008,#9009,#9010,#9011,#9012,#9013,
#9014,#9015,#9016,#9017,#9018,#9019,#9020,#9021,#9022,#9023),(#9024,#9025,
#9026,#9027,#9028,#9029,#9030,#9031,#9032,#9033,#9034,#9035,#9036,#9037,
#9038,#9039,#9040,#9041,#9042,#9043,#9044,#9045,#9046,#9047,#9048,#9049,
#9050,#9051,#9052,#9053,#9054,#9055,#9056,#9057,#9058,#9059,#9060,#9061,
#9062,#9063,#9064,#9065,#9066,#9067,#9068,#9069,#9070,#9071,#9072,#9073,
#9074,#9075,#9076,#9077,#9078,#9079,#9080,#9081,#9082,#9083,#9084,#9085,
#9086,#9087,#9088,#9089,#9090,#9091,#9092,#9093,#9094,#9095,#9096,#9097,
#9098,#9099,#9100)),.UNSPECIFIED.,.F.,.F.,.F.,(4,4),(4,1,1,1,1,1,1,1,1,
1,1,1,1,1,1,1,1,1,1,1,1,1,1,1,1,1,1,1,1,1,1,1,1,1,1,1,1,1,1,1,1,1,1,1,1,
1,1,1,1,1,1,1,1,1,1,1,1,1,1,1,1,1,1,1,1,1,1,1,1,1,1,1,1,1,4),(0.,0.0658467982010768),
(11.6150328478182,12.6023632471184,13.5896936464185,14.5770240457187,15.5643544450188,
16.551684844319,17.5390152436191,18.5263456429193,19.5136760422194,20.5010064415196,
21.4883368408197,22.4756672401199,23.46299763942,24.4503280387202,25.4376584380203,
26.4249888373205,27.4123192366206,28.3996496359208,29.3869800352209,30.3743104345211,
31.3616408338212,32.3489712331214,33.3363016324215,34.3236320317217,35.3109624310218,
36.298292830322,37.2856232296221,38.2729536289223,39.2602840282224,40.2476144275226,
41.2349448268227,42.2222752261229,43.209605625423,44.1969360247232,45.1842664240233,
46.1715968233235,47.1589272226236,48.1462576219238,49.1335880212239,50.1209184205241,
51.1082488198242,52.0955792191244,53.0829096184245,54.0702400177247,55.0575704170248,
56.0449008163249,57.0322312156251,58.0195616149252,59.0068920142254,59.9942224135255,
60.9815528128257,61.9688832121258,62.956213611426,63.9435440107261,64.9308744100263,
65.9182048093264,66.9055352086266,67.8928656079267,68.8801960072269,69.867526406527,
70.8548568058272,71.8421872051273,72.8295176044275,73.8168480037276,74.8041784030278,
75.7915088023279,76.7788392016281,77.7661696009282,78.7535000002284,79.7408303995285,
80.7281607988287,81.7154911981288,82.702821597429,83.6901519967291,84.6774823960293),
 .UNSPECIFIED.);
#215=B_SPLINE_SURFACE_WITH_KNOTS('',3,3,((#9229,#9230,#9231,#9232,#9233,
#9234,#9235,#9236,#9237,#9238,#9239,#9240,#9241,#9242,#9243,#9244,#9245,
#9246,#9247,#9248,#9249,#9250,#9251,#9252,#9253,#9254,#9255,#9256,#9257,
#9258,#9259,#9260,#9261,#9262,#9263,#9264,#9265,#9266,#9267,#9268,#9269,
#9270,#9271,#9272,#9273,#9274,#9275,#9276,#9277,#9278,#9279,#9280,#9281,
#9282,#9283,#9284,#9285,#9286,#9287,#9288,#9289,#9290,#9291,#9292,#9293,
#9294,#9295,#9296,#9297,#9298,#9299,#9300,#9301,#9302,#9303,#9304,#9305,
#9306,#9307),(#9308,#9309,#9310,#9311,#9312,#9313,#9314,#9315,#9316,#9317,
#9318,#9319,#9320,#9321,#9322,#9323,#9324,#9325,#9326,#9327,#9328,#9329,
#9330,#9331,#9332,#9333,#9334,#9335,#9336,#9337,#9338,#9339,#9340,#9341,
#9342,#9343,#9344,#9345,#9346,#9347,#9348,#9349,#9350,#9351,#9352,#9353,
#9354,#9355,#9356,#9357,#9358,#9359,#9360,#9361,#9362,#9363,#9364,#9365,
#9366,#9367,#9368,#9369,#9370,#9371,#9372,#9373,#9374,#9375,#9376,#9377,
#9378,#9379,#9380,#9381,#9382,#9383,#9384,#9385,#9386),(#9387,#9388,#9389,
#9390,#9391,#9392,#9393,#9394,#9395,#9396,#9397,#9398,#9399,#9400,#9401,
#9402,#9403,#9404,#9405,#9406,#9407,#9408,#9409,#9410,#9411,#9412,#9413,
#9414,#9415,#9416,#9417,#9418,#9419,#9420,#9421,#9422,#9423,#9424,#9425,
#9426,#9427,#9428,#9429,#9430,#9431,#9432,#9433,#9434,#9435,#9436,#9437,
#9438,#9439,#9440,#9441,#9442,#9443,#9444,#9445,#9446,#9447,#9448,#9449,
#9450,#9451,#9452,#9453,#9454,#9455,#9456,#9457,#9458,#9459,#9460,#9461,
#9462,#9463,#9464,#9465),(#9466,#9467,#9468,#9469,#9470,#9471,#9472,#9473,
#9474,#9475,#9476,#9477,#9478,#9479,#9480,#9481,#9482,#9483,#9484,#9485,
#9486,#9487,#9488,#9489,#9490,#9491,#9492,#9493,#9494,#9495,#9496,#9497,
#9498,#9499,#9500,#9501,#9502,#9503,#9504,#9505,#9506,#9507,#9508,#9509,
#9510,#9511,#9512,#9513,#9514,#9515,#9516,#9517,#9518,#9519,#9520,#9521,
#9522,#9523,#9524,#9525,#9526,#9527,#9528,#9529,#9530,#9531,#9532,#9533,
#9534,#9535,#9536,#9537,#9538,#9539,#9540,#9541,#9542,#9543,#9544)),
 .UNSPECIFIED.,.F.,.F.,.F.,(4,4),(4,1,1,1,1,1,1,1,1,1,1,1,1,1,1,1,1,1,1,
1,1,1,1,1,1,1,1,1,1,1,1,1,1,1,1,1,1,1,1,1,1,1,1,1,1,1,1,1,1,1,1,1,1,1,1,
1,1,1,1,1,1,1,1,1,1,1,1,1,1,1,1,1,1,1,1,1,4),(0.,0.0658467982010768),(8.30747755240104,
9.2960444961263,10.2846114398516,11.2731783835768,12.2617453273021,13.2503122710274,
14.2388792147526,15.2274461584779,16.2160131022032,17.2045800459284,18.1931469896537,
19.181713933379,20.1702808771042,21.1588478208295,22.1474147645547,23.13598170828,
24.1245486520053,25.1131155957305,26.1016825394558,27.0902494831811,28.0788164269063,
29.0673833706316,30.0559503143569,31.0445172580821,32.0330842018074,33.0216511455327,
34.0102180892579,34.9987850329832,35.9873519767085,36.9759189204337,37.964485864159,
38.9530528078842,39.9416197516095,40.9301866953348,41.91875363906,42.9073205827853,
43.8958875265106,44.8844544702358,45.8730214139611,46.8615883576864,47.8501553014116,
48.8387222451369,49.8272891888622,50.8158561325874,51.8044230763127,52.792990020038,
53.7815569637632,54.7701239074885,55.7586908512138,56.747257794939,57.7358247386643,
58.7243916823895,59.7129586261148,60.7015255698401,61.6900925135653,62.6786594572906,
63.6672264010159,64.6557933447411,65.6443602884664,66.6329272321917,67.6214941759169,
68.6100611196422,69.5986280633675,70.5871950070927,71.575761950818,72.5643288945433,
73.5528958382685,74.5414627819938,75.530029725719,76.5185966694443,77.5071636131696,
78.4957305568948,79.4842975006201,80.4728644443454,81.4614313880706,82.4499983317959,
83.4385652755212),.UNSPECIFIED.);
#260=B_SPLINE_CURVE_WITH_KNOTS('',3,(#7687,#7688,#7689,#7690,#7691,#7692,
#7693,#7694,#7695,#7696),.UNSPECIFIED.,.F.,.F.,(4,3,3,4),(-4.09293042013066,
-3.9493215972006,-2.96199119790045,-2.06863817490914),.UNSPECIFIED.);
#261=B_SPLINE_CURVE_WITH_KNOTS('',3,(#7699,#7700,#7701,#7702,#7703,#7704,
#7705),.UNSPECIFIED.,.F.,.F.,(4,3,4),(0.,0.988566943725272,1.11730040836823),
 .UNSPECIFIED.);
#262=B_SPLINE_CURVE_WITH_KNOTS('',3,(#7710,#7711,#7712,#7713,#7714,#7715,
#7716,#7717,#7718,#7719,#7720,#7721,#7722,#7723,#7724,#7725,#7726,#7727,
#7728,#7729,#7730,#7731),.UNSPECIFIED.,.F.,.F.,(4,3,3,3,3,3,3,4),(-10.3761157273102,
-9.87330399300149,-8.88597359370134,-7.89864319440119,-6.91131279510104,
-5.92398239580089,-4.93665199650074,-4.09293042013066),.UNSPECIFIED.);
#263=B_SPLINE_CURVE_WITH_KNOTS('',3,(#7732,#7733,#7734,#7735,#7736,#7737,
#7738,#7739,#7740,#7741,#7742,#7743,#7744,#7745,#7746,#7747,#7748,#7749,
#7750,#7751,#7752,#7753),.UNSPECIFIED.,.F.,.F.,(4,3,3,3,3,3,3,4),(1.11730040836823,
1.97713388745054,2.9657008311758,3.95426777490106,4.94283471862632,5.93140166235159,
6.91996860607685,7.40048571554782),.UNSPECIFIED.);
#264=B_SPLINE_CURVE_WITH_KNOTS('',3,(#7758,#7759,#7760,#7761,#7762,#7763,
#7764,#7765,#7766,#7767,#7768,#7769,#7770,#7771,#7772,#7773,#7774,#7775,
#7776,#7777,#7778,#7779),.UNSPECIFIED.,.F.,.F.,(4,3,3,3,3,3,3,4),(-16.6593010344898,
-15.7972863888024,-14.8099559895022,-13.8226255902021,-12.8352951909019,
-11.8479647916018,-10.8606343923016,-10.3761157273102),.UNSPECIFIED.);
#265=B_SPLINE_CURVE_WITH_KNOTS('',3,(#7780,#7781,#7782,#7783,#7784,#7785,
#7786,#7787,#7788,#7789,#7790,#7791,#7792,#7793,#7794,#7795,#7796,#7797,
#7798,#7799,#7800,#7801),.UNSPECIFIED.,.F.,.F.,(4,3,3,3,3,3,3,4),(7.40048571554782,
7.90853554980211,8.89710249352738,9.88566943725264,10.8742363809779,11.8628033247032,
12.8513702684284,13.6836710227274),.UNSPECIFIED.);
#266=B_SPLINE_CURVE_WITH_KNOTS('',3,(#7806,#7807,#7808,#7809,#7810,#7811,
#7812,#7813,#7814,#7815,#7816,#7817,#7818,#7819,#7820,#7821,#7822,#7823,
#7824,#7825,#7826,#7827,#7828,#7829,#7830),.UNSPECIFIED.,.F.,.F.,(4,3,3,
3,3,3,3,3,4),(-22.9424863416694,-22.7085991839034,-21.7212687846033,-20.7339383853031,
-19.746607986003,-18.7592775867028,-17.7719471874027,-16.7846167881025,
-16.6593010344898),.UNSPECIFIED.);
#267=B_SPLINE_CURVE_WITH_KNOTS('',3,(#7831,#7832,#7833,#7834,#7835,#7836,
#7837,#7838,#7839,#7840,#7841,#7842,#7843,#7844,#7845,#7846,#7847,#7848,
#7849,#7850,#7851,#7852,#7853,#7854,#7855),.UNSPECIFIED.,.F.,.F.,(4,3,3,
3,3,3,3,3,4),(13.6836710227274,13.8399372121537,14.828504155879,15.8170710996042,
16.8056380433295,17.7942049870548,18.78277193078,19.7713388745053,19.966856329907),
 .UNSPECIFIED.);
#268=B_SPLINE_CURVE_WITH_KNOTS('',3,(#7860,#7861,#7862,#7863,#7864,#7865,
#7866,#7867,#7868,#7869,#7870,#7871,#7872,#7873,#7874,#7875,#7876,#7877,
#7878,#7879,#7880,#7881),.UNSPECIFIED.,.F.,.F.,(4,3,3,3,3,3,3,4),(-29.225671648849,
-28.6325815797043,-27.6452511804042,-26.657920781104,-25.6705903818039,
-24.6832599825037,-23.6959295832036,-22.9424863416694),.UNSPECIFIED.);
#269=B_SPLINE_CURVE_WITH_KNOTS('',3,(#7882,#7883,#7884,#7885,#7886,#7887,
#7888,#7889,#7890,#7891,#7892,#7893,#7894,#7895,#7896,#7897,#7898,#7899,
#7900,#7901,#7902,#7903),.UNSPECIFIED.,.F.,.F.,(4,3,3,3,3,3,3,4),(19.966856329907,
20.7599058182306,21.7484727619558,22.7370397056811,23.7256066494064,24.7141735931316,
25.7027405368569,26.2500416370866),.UNSPECIFIED.);
#270=B_SPLINE_CURVE_WITH_KNOTS('',3,(#7908,#7909,#7910,#7911,#7912,#7913,
#7914,#7915,#7916,#7917,#7918,#7919,#7920,#7921,#7922,#7923,#7924,#7925,
#7926,#7927,#7928,#7929),.UNSPECIFIED.,.F.,.F.,(4,3,3,3,3,3,3,4),(-35.5088569560286,
-34.5565639755052,-33.5692335762051,-32.5819031769049,-31.5945727776048,
-30.6072423783046,-29.6199119790045,-29.225671648849),.UNSPECIFIED.);
#271=B_SPLINE_CURVE_WITH_KNOTS('',3,(#7930,#7931,#7932,#7933,#7934,#7935,
#7936,#7937,#7938,#7939,#7940,#7941,#7942,#7943,#7944,#7945,#7946,#7947,
#7948,#7949,#7950,#7951),.UNSPECIFIED.,.F.,.F.,(4,3,3,3,3,3,3,4),(26.2500416370866,
26.6913074805822,27.6798744243074,28.6684413680327,29.6570083117579,30.6455752554832,
31.6341421992085,32.5332269442662),.UNSPECIFIED.);
#272=B_SPLINE_CURVE_WITH_KNOTS('',3,(#7956,#7957,#7958,#7959,#7960,#7961,
#7962,#7963,#7964,#7965,#7966,#7967,#7968,#7969,#7970,#7971,#7972,#7973,
#7974,#7975,#7976,#7977,#7978,#7979,#7980),.UNSPECIFIED.,.F.,.F.,(4,3,3,
3,3,3,3,3,4),(-41.7920422632082,-41.4678767706063,-40.4805463713061,-39.4932159720059,
-38.5058855727058,-37.5185551734057,-36.5312247741055,-35.5438943748054,
-35.5088569560286),.UNSPECIFIED.);
#273=B_SPLINE_CURVE_WITH_KNOTS('',3,(#7981,#7982,#7983,#7984,#7985,#7986,
#7987,#7988,#7989,#7990,#7991,#7992,#7993,#7994,#7995,#7996,#7997,#7998,
#7999,#8000,#8001,#8002,#8003,#8004,#8005),.UNSPECIFIED.,.F.,.F.,(4,3,3,
3,3,3,3,3,4),(32.5332269442662,32.6227091429337,33.611276086659,34.5998430303843,
35.5884099741095,36.5769769178348,37.5655438615601,38.5541108052853,38.8164122514458),
 .UNSPECIFIED.);
#274=B_SPLINE_CURVE_WITH_KNOTS('',3,(#8010,#8011,#8012,#8013,#8014,#8015,
#8016,#8017,#8018,#8019,#8020,#8021,#8022,#8023,#8024,#8025,#8026,#8027,
#8028,#8029,#8030,#8031),.UNSPECIFIED.,.F.,.F.,(4,3,3,3,3,3,3,4),(-48.0752275703878,
-47.3918591664071,-46.404528767107,-45.4171983678069,-44.4298679685067,
-43.4425375692066,-42.4552071699064,-41.7920422632082),.UNSPECIFIED.);
#275=B_SPLINE_CURVE_WITH_KNOTS('',3,(#8032,#8033,#8034,#8035,#8036,#8037,
#8038,#8039,#8040,#8041,#8042,#8043,#8044,#8045,#8046,#8047,#8048,#8049,
#8050,#8051,#8052,#8053),.UNSPECIFIED.,.F.,.F.,(4,3,3,3,3,3,3,4),(38.8164122514458,
39.5426777490106,40.5312446927359,41.5198116364611,42.5083785801864,43.4969455239117,
44.4855124676369,45.0995975586253),.UNSPECIFIED.);
#276=B_SPLINE_CURVE_WITH_KNOTS('',3,(#8058,#8059,#8060,#8061,#8062,#8063,
#8064,#8065,#8066,#8067,#8068,#8069,#8070,#8071,#8072,#8073,#8074,#8075,
#8076,#8077,#8078,#8079,#8080,#8081,#8082),.UNSPECIFIED.,.F.,.F.,(4,3,3,
3,3,3,3,3,4),(-54.3584128775674,-54.3031719615082,-53.315841562208,-52.3285111629079,
-51.3411807636077,-50.3538503643076,-49.3665199650074,-48.3791895657073,
-48.0752275703878),.UNSPECIFIED.);
#277=B_SPLINE_CURVE_WITH_KNOTS('',3,(#8083,#8084,#8085,#8086,#8087,#8088,
#8089,#8090,#8091,#8092,#8093,#8094,#8095,#8096,#8097,#8098,#8099,#8100,
#8101,#8102,#8103,#8104),.UNSPECIFIED.,.F.,.F.,(4,3,3,3,3,3,3,4),(45.0995975586253,
45.4740794113622,46.4626463550875,47.4512132988127,48.439780242538,49.4283471862633,
50.4169141299885,51.3827828658049),.UNSPECIFIED.);
#278=B_SPLINE_CURVE_WITH_KNOTS('',3,(#8109,#8110,#8111,#8112,#8113,#8114,
#8115,#8116,#8117,#8118,#8119,#8120,#8121,#8122,#8123,#8124,#8125,#8126,
#8127,#8128,#8129,#8130),.UNSPECIFIED.,.F.,.F.,(4,3,3,3,3,3,3,4),(-60.641598184747,
-60.2271543573091,-59.2398239580089,-58.2524935587088,-57.2651631594086,
-56.2778327601085,-55.2905023608083,-54.3584128775674),.UNSPECIFIED.);
#279=B_SPLINE_CURVE_WITH_KNOTS('',3,(#8131,#8132,#8133,#8134,#8135,#8136,
#8137,#8138,#8139,#8140,#8141,#8142,#8143,#8144,#8145,#8146,#8147,#8148,
#8149,#8150,#8151,#8152,#8153,#8154,#8155),.UNSPECIFIED.,.F.,.F.,(4,3,3,
3,3,3,3,3,4),(51.3827828658049,51.4054810737138,52.394048017439,53.3826149611643,
54.3711819048896,55.3597488486148,56.3483157923401,57.3368827360654,57.6659681729845),
 .UNSPECIFIED.);
#280=B_SPLINE_CURVE_WITH_KNOTS('',3,(#8160,#8161,#8162,#8163,#8164,#8165,
#8166,#8167,#8168,#8169,#8170,#8171,#8172,#8173,#8174,#8175,#8176,#8177,
#8178,#8179,#8180,#8181),.UNSPECIFIED.,.F.,.F.,(4,3,3,3,3,3,3,4),(-66.9247834919266,
-66.15113675311,-65.1638063538098,-64.1764759545097,-63.1891455552095,-62.2018151559094,
-61.2144847566092,-60.641598184747),.UNSPECIFIED.);
#281=B_SPLINE_CURVE_WITH_KNOTS('',3,(#8182,#8183,#8184,#8185,#8186,#8187,
#8188,#8189,#8190,#8191,#8192,#8193,#8194,#8195,#8196,#8197,#8198,#8199,
#8200,#8201,#8202,#8203),.UNSPECIFIED.,.F.,.F.,(4,3,3,3,3,3,3,4),(57.6659681729845,
58.3254496797906,59.3140166235159,60.3025835672412,61.2911505109664,62.2797174546917,
63.268284398417,63.9491534801641),.UNSPECIFIED.);
#282=B_SPLINE_CURVE_WITH_KNOTS('',3,(#8209,#8210,#8211,#8212,#8213,#8214,
#8215,#8216,#8217,#8218),.UNSPECIFIED.,.F.,.F.,(4,1,1,1,1,1,1,4),(78.5398163397448,
78.7535000002284,79.7408303995285,80.7281607988287,81.7154911981288,82.702821597429,
83.6901519967291,84.6774823960293),.UNSPECIFIED.);
#283=B_SPLINE_CURVE_WITH_KNOTS('',3,(#8221,#8222,#8223,#8224,#8225,#8226,
#8227,#8228),.UNSPECIFIED.,.F.,.F.,(4,1,1,1,1,4),(78.5398163397448,79.4842975006201,
80.4728644443454,81.4614313880706,82.4499983317959,83.4385652755212),
 .UNSPECIFIED.);
#284=B_SPLINE_CURVE_WITH_KNOTS('',3,(#8233,#8234,#8235,#8236,#8237,#8238,
#8239,#8240,#8241,#8242),.UNSPECIFIED.,.F.,.F.,(4,1,1,1,1,1,1,4),(72.2566310325653,
72.8295176044275,73.8168480037276,74.8041784030278,75.7915088023279,76.7788392016281,
77.7661696009282,78.5398163397448),.UNSPECIFIED.);
#285=B_SPLINE_CURVE_WITH_KNOTS('',3,(#8243,#8244,#8245,#8246,#8247,#8248,
#8249,#8250,#8251,#8252,#8253),.UNSPECIFIED.,.F.,.F.,(4,1,1,1,1,1,1,1,4),
(72.2566310325652,72.5643288945433,73.5528958382685,74.5414627819938,75.530029725719,
76.5185966694443,77.5071636131696,78.4957305568948,78.5398163397448),
 .UNSPECIFIED.);
#286=B_SPLINE_CURVE_WITH_KNOTS('',3,(#8258,#8259,#8260,#8261,#8262,#8263,
#8264,#8265,#8266,#8267),.UNSPECIFIED.,.F.,.F.,(4,1,1,1,1,1,1,4),(65.9734457253856,
66.9055352086266,67.8928656079267,68.8801960072269,69.867526406527,70.8548568058272,
71.8421872051273,72.2566310325653),.UNSPECIFIED.);
#287=B_SPLINE_CURVE_WITH_KNOTS('',3,(#8268,#8269,#8270,#8271,#8272,#8273,
#8274,#8275,#8276,#8277),.UNSPECIFIED.,.F.,.F.,(4,1,1,1,1,1,1,4),(65.9734457253856,
66.6329272321917,67.6214941759169,68.6100611196422,69.5986280633675,70.5871950070927,
71.575761950818,72.2566310325652),.UNSPECIFIED.);
#288=B_SPLINE_CURVE_WITH_KNOTS('',3,(#8282,#8283,#8284,#8285,#8286,#8287,
#8288,#8289,#8290,#8291,#8292),.UNSPECIFIED.,.F.,.F.,(4,1,1,1,1,1,1,1,4),
(59.6902604182061,59.9942224135255,60.9815528128257,61.9688832121258,62.956213611426,
63.9435440107261,64.9308744100263,65.9182048093264,65.9734457253856),
 .UNSPECIFIED.);
#289=B_SPLINE_CURVE_WITH_KNOTS('',3,(#8293,#8294,#8295,#8296,#8297,#8298,
#8299,#8300,#8301,#8302,#8303),.UNSPECIFIED.,.F.,.F.,(4,1,1,1,1,1,1,1,4),
(59.6902604182061,59.7129586261148,60.7015255698401,61.6900925135653,62.6786594572906,
63.6672264010159,64.6557933447411,65.6443602884664,65.9734457253856),
 .UNSPECIFIED.);
#290=B_SPLINE_CURVE_WITH_KNOTS('',3,(#8308,#8309,#8310,#8311,#8312,#8313,
#8314,#8315,#8316,#8317),.UNSPECIFIED.,.F.,.F.,(4,1,1,1,1,1,1,4),(53.4070751110265,
54.0702400177247,55.0575704170248,56.0449008163249,57.0322312156251,58.0195616149252,
59.0068920142254,59.6902604182061),.UNSPECIFIED.);
#291=B_SPLINE_CURVE_WITH_KNOTS('',3,(#8318,#8319,#8320,#8321,#8322,#8323,
#8324,#8325,#8326,#8327),.UNSPECIFIED.,.F.,.F.,(4,1,1,1,1,1,1,4),(53.4070751110265,
53.7815569637632,54.7701239074885,55.7586908512138,56.747257794939,57.7358247386643,
58.7243916823895,59.6902604182061),.UNSPECIFIED.);
#292=B_SPLINE_CURVE_WITH_KNOTS('',3,(#8332,#8333,#8334,#8335,#8336,#8337,
#8338,#8339,#8340,#8341,#8342),.UNSPECIFIED.,.F.,.F.,(4,1,1,1,1,1,1,1,4),
(47.1238898038469,47.1589272226236,48.1462576219238,49.1335880212239,50.1209184205241,
51.1082488198242,52.0955792191244,53.0829096184245,53.4070751110265),
 .UNSPECIFIED.);
#293=B_SPLINE_CURVE_WITH_KNOTS('',3,(#8343,#8344,#8345,#8346,#8347,#8348,
#8349,#8350,#8351,#8352),.UNSPECIFIED.,.F.,.F.,(4,1,1,1,1,1,1,4),(47.1238898038469,
47.8501553014116,48.8387222451369,49.8272891888622,50.8158561325874,51.8044230763127,
52.792990020038,53.4070751110265),.UNSPECIFIED.);
#294=B_SPLINE_CURVE_WITH_KNOTS('',3,(#8357,#8358,#8359,#8360,#8361,#8362,
#8363,#8364,#8365,#8366),.UNSPECIFIED.,.F.,.F.,(4,1,1,1,1,1,1,4),(40.8407044966673,
41.2349448268227,42.2222752261229,43.209605625423,44.1969360247232,45.1842664240233,
46.1715968233235,47.1238898038469),.UNSPECIFIED.);
#295=B_SPLINE_CURVE_WITH_KNOTS('',3,(#8367,#8368,#8369,#8370,#8371,#8372,
#8373,#8374,#8375,#8376,#8377),.UNSPECIFIED.,.F.,.F.,(4,1,1,1,1,1,1,1,4),
(40.8407044966673,40.9301866953348,41.91875363906,42.9073205827853,43.8958875265106,
44.8844544702358,45.8730214139611,46.8615883576864,47.1238898038469),
 .UNSPECIFIED.);
#296=B_SPLINE_CURVE_WITH_KNOTS('',3,(#8382,#8383,#8384,#8385,#8386,#8387,
#8388,#8389,#8390,#8391),.UNSPECIFIED.,.F.,.F.,(4,1,1,1,1,1,1,4),(34.5575191894877,
35.3109624310218,36.298292830322,37.2856232296221,38.2729536289223,39.2602840282224,
40.2476144275226,40.8407044966673),.UNSPECIFIED.);
#297=B_SPLINE_CURVE_WITH_KNOTS('',3,(#8392,#8393,#8394,#8395,#8396,#8397,
#8398,#8399,#8400,#8401),.UNSPECIFIED.,.F.,.F.,(4,1,1,1,1,1,1,4),(34.5575191894877,
34.9987850329832,35.9873519767085,36.9759189204337,37.964485864159,38.9530528078842,
39.9416197516095,40.8407044966673),.UNSPECIFIED.);
#298=B_SPLINE_CURVE_WITH_KNOTS('',3,(#8406,#8407,#8408,#8409,#8410,#8411,
#8412,#8413,#8414,#8415,#8416),.UNSPECIFIED.,.F.,.F.,(4,1,1,1,1,1,1,1,4),
(28.2743338823081,28.3996496359208,29.3869800352209,30.3743104345211,31.3616408338212,
32.3489712331214,33.3363016324215,34.3236320317217,34.5575191894877),
 .UNSPECIFIED.);
#299=B_SPLINE_CURVE_WITH_KNOTS('',3,(#8417,#8418,#8419,#8420,#8421,#8422,
#8423,#8424,#8425,#8426),.UNSPECIFIED.,.F.,.F.,(4,1,1,1,1,1,1,4),(28.2743338823081,
29.0673833706316,30.0559503143569,31.0445172580821,32.0330842018074,33.0216511455327,
34.0102180892579,34.5575191894877),.UNSPECIFIED.);
#300=B_SPLINE_CURVE_WITH_KNOTS('',3,(#8431,#8432,#8433,#8434,#8435,#8436,
#8437,#8438,#8439,#8440),.UNSPECIFIED.,.F.,.F.,(4,1,1,1,1,1,1,4),(21.9911485751285,
22.4756672401199,23.46299763942,24.4503280387202,25.4376584380203,26.4249888373205,
27.4123192366206,28.2743338823081),.UNSPECIFIED.);
#301=B_SPLINE_CURVE_WITH_KNOTS('',3,(#8441,#8442,#8443,#8444,#8445,#8446,
#8447,#8448,#8449,#8450,#8451),.UNSPECIFIED.,.F.,.F.,(4,1,1,1,1,1,1,1,4),
(21.9911485751285,22.1474147645547,23.13598170828,24.1245486520053,25.1131155957305,
26.1016825394558,27.0902494831811,28.0788164269063,28.2743338823081),
 .UNSPECIFIED.);
#302=B_SPLINE_CURVE_WITH_KNOTS('',3,(#8456,#8457,#8458,#8459,#8460,#8461,
#8462,#8463,#8464,#8465),.UNSPECIFIED.,.F.,.F.,(4,1,1,1,1,1,1,4),(15.7079632679489,
16.551684844319,17.5390152436191,18.5263456429193,19.5136760422194,20.5010064415196,
21.4883368408197,21.9911485751285),.UNSPECIFIED.);
#303=B_SPLINE_CURVE_WITH_KNOTS('',3,(#8466,#8467,#8468,#8469,#8470,#8471,
#8472,#8473,#8474,#8475),.UNSPECIFIED.,.F.,.F.,(4,1,1,1,1,1,1,4),(15.7079632679489,
16.2160131022032,17.2045800459284,18.1931469896537,19.181713933379,20.1702808771042,
21.1588478208295,21.9911485751285),.UNSPECIFIED.);
#304=B_SPLINE_CURVE_WITH_KNOTS('',3,(#8478,#8479,#8480,#8481,#8482,#8483,
#8484,#8485,#8486,#8487,#8488,#8489,#8490,#8491,#8492,#8493,#8494,#8495,
#8496,#8497,#8498,#8499,#8500,#8501,#8502,#8503,#8504,#8505,#8506,#8507,
#8508,#8509,#8510,#8511,#8512,#8513,#8514,#8515,#8516,#8517,#8518,#8519,
#8520,#8521,#8522,#8523,#8524,#8525,#8526,#8527,#8528,#8529,#8530,#8531,
#8532,#8533,#8534,#8535,#8536,#8537,#8538,#8539,#8540,#8541,#8542,#8543,
#8544,#8545,#8546,#8547,#8548,#8549,#8550,#8551,#8552,#8553,#8554,#8555,
#8556,#8557,#8558,#8559,#8560,#8561,#8562,#8563,#8564,#8565,#8566,#8567,
#8568,#8569,#8570,#8571,#8572,#8573,#8574,#8575,#8576,#8577,#8578,#8579,
#8580,#8581,#8582,#8583,#8584,#8585,#8586,#8587,#8588,#8589,#8590,#8591,
#8592,#8593,#8594,#8595,#8596,#8597,#8598,#8599,#8600,#8601,#8602,#8603,
#8604,#8605,#8606,#8607,#8608,#8609,#8610,#8611,#8612,#8613,#8614,#8615,
#8616,#8617,#8618,#8619,#8620,#8621,#8622,#8623,#8624,#8625,#8626,#8627,
#8628,#8629,#8630,#8631,#8632,#8633,#8634,#8635,#8636,#8637,#8638,#8639,
#8640,#8641,#8642,#8643,#8644,#8645,#8646,#8647,#8648,#8649,#8650,#8651,
#8652,#8653,#8654,#8655,#8656,#8657,#8658,#8659,#8660,#8661,#8662,#8663,
#8664,#8665,#8666,#8667,#8668,#8669,#8670,#8671,#8672,#8673,#8674,#8675,
#8676,#8677,#8678,#8679,#8680,#8681,#8682,#8683,#8684,#8685,#8686,#8687,
#8688,#8689,#8690,#8691,#8692,#8693,#8694),.UNSPECIFIED.,.F.,.F.,(4,3,3,
3,3,3,3,3,3,3,3,3,3,3,3,3,3,3,3,3,3,3,3,3,3,3,3,3,3,3,3,3,3,3,3,3,3,3,3,
3,3,3,3,3,3,3,3,3,3,3,3,3,3,3,3,3,3,3,3,3,3,3,3,3,3,3,3,3,3,3,3,3,4),(-1.51155304937228,
-1.48679174718013,-1.46137597198077,-1.44942691521821,-1.44205848651244,
-1.43724119559823,-1.41130764113729,-1.38514768961224,-1.36936593028954,
-1.36512230166791,-1.33867581137855,-1.31235917608035,-1.29127511993008,
-1.28073309185494,-1.2739086628828,-1.27019106377981,-1.24488979836553,
-1.21884130205047,-1.19384888620637,-1.18291470427457,-1.17641188206357,
-1.17130697868968,-1.14451640582175,-1.11742561305122,-1.09279470361283,
-1.08177565945417,-1.07670730294613,-1.07245364414871,-1.0452101587782,
-1.01890197529764,-0.992076665792053,-0.977095538498891,-0.971310437727824,
-0.944262984582137,-0.91671696123902,-0.889051349044572,-0.8786107219546,
-0.873404326505122,-0.869185758667877,-0.841205731090746,-0.813331817877821,
-0.785648584359967,-0.771436006282574,-0.765308450445371,-0.757965350842113,
-0.731019445974318,-0.703340715547858,-0.676331238706378,-0.668063308133434,
-0.663247880961674,-0.658967945513649,-0.630690110839631,-0.602089962339152,
-0.573383696958367,-0.562618847440572,-0.556352694911719,-0.55203012393032,
-0.523164492059728,-0.494713544949419,-0.487264900816012,-0.45884309987075,
-0.449622389577847,-0.445165938771905,-0.416742684601646,-0.387755299334011,
-0.358563756837841,-0.34211828207705,-0.337697582134308,-0.308241853281341,
-0.278784672736061,-0.25000255453776,-0.226999958751515,-0.219677966288006),
 .UNSPECIFIED.);
#305=B_SPLINE_CURVE_WITH_KNOTS('',3,(#8696,#8697,#8698,#8699,#8700,#8701,
#8702,#8703,#8704,#8705,#8706,#8707,#8708,#8709,#8710,#8711,#8712,#8713,
#8714,#8715,#8716,#8717,#8718,#8719,#8720,#8721,#8722,#8723,#8724,#8725,
#8726,#8727,#8728,#8729,#8730,#8731,#8732,#8733,#8734,#8735,#8736,#8737,
#8738,#8739,#8740,#8741,#8742,#8743,#8744,#8745,#8746,#8747,#8748,#8749,
#8750,#8751,#8752,#8753,#8754,#8755,#8756),.UNSPECIFIED.,.F.,.F.,(4,3,3,
3,3,3,3,3,3,3,3,3,3,3,3,3,3,3,3,3,4),(-0.410648750432938,-0.381294613665594,
-0.352267124576947,-0.328792823836752,-0.311187098281605,-0.306018425011984,
-0.301691296836585,-0.274143229574461,-0.258369921616165,-0.230117472373342,
-0.201352788326674,-0.195525900786732,-0.16833922287309,-0.141249160586392,
-0.114615533759621,-0.100282139063474,-0.0960342097686789,-0.0702554174629941,
-0.0448546715641945,-0.0201984500449382,0.),.UNSPECIFIED.);
#306=B_SPLINE_CURVE_WITH_KNOTS('',3,(#8759,#8760,#8761,#8762,#8763,#8764,
#8765,#8766,#8767,#8768,#8769,#8770,#8771,#8772,#8773,#8774,#8775,#8776,
#8777,#8778,#8779,#8780,#8781,#8782,#8783,#8784,#8785,#8786,#8787,#8788,
#8789),.UNSPECIFIED.,.F.,.F.,(4,3,3,3,3,3,3,3,3,3,4),(-0.219677966288006,
-0.206985183547511,-0.178213580556878,-0.148819200354015,-0.130216800309763,
-0.118450459252591,-0.113866160083042,-0.0841488051349767,-0.0540951018364117,
-0.0242019686830237,0.),.UNSPECIFIED.);
#307=B_SPLINE_CURVE_WITH_KNOTS('',3,(#9102,#9103,#9104,#9105,#9106,#9107,
#9108,#9109),.UNSPECIFIED.,.F.,.F.,(4,1,1,1,1,4),(11.6150328478182,12.6023632471184,
13.5896936464185,14.5770240457187,15.5643544450188,15.7079632679489),
 .UNSPECIFIED.);
#308=B_SPLINE_CURVE_WITH_KNOTS('',3,(#9110,#9111,#9112,#9113,#9114,#9115,
#9116,#9117,#9118,#9119,#9120,#9121,#9122,#9123,#9124,#9125,#9126,#9127,
#9128,#9129,#9130,#9131,#9132,#9133,#9134,#9135,#9136,#9137,#9138,#9139,
#9140,#9141,#9142,#9143,#9144,#9145,#9146,#9147,#9148,#9149,#9150,#9151,
#9152,#9153,#9154,#9155,#9156,#9157,#9158,#9159,#9160,#9161,#9162,#9163,
#9164,#9165,#9166,#9167,#9168,#9169,#9170,#9171,#9172,#9173,#9174,#9175,
#9176,#9177,#9178,#9179,#9180,#9181,#9182,#9183,#9184,#9185,#9186,#9187,
#9188,#9189,#9190,#9191,#9192,#9193,#9194,#9195,#9196,#9197),
 .UNSPECIFIED.,.F.,.F.,(4,3,3,3,3,3,3,3,3,3,3,3,3,3,3,3,3,3,3,3,3,3,3,3,
3,3,3,3,3,4),(-0.55274537837504,-0.525174630400016,-0.495740003900857,-0.479498227927527,
-0.472105972866577,-0.443064611280178,-0.418881458903182,-0.408301329738247,
-0.401969450637142,-0.397429868442983,-0.369124488132221,-0.341064938672273,
-0.313899750226951,-0.29772704364586,-0.291366968188088,-0.264559598151202,
-0.249599392264211,-0.222215347947115,-0.194438429453726,-0.189292991414398,
-0.162670593649827,-0.136062352557756,-0.109859916217256,-0.101879142728474,
-0.0950850259724172,-0.09115324392662,-0.0655931049079899,-0.0404250325776628,
-0.0160423336449029,0.),.UNSPECIFIED.);
#309=B_SPLINE_CURVE_WITH_KNOTS('',3,(#9198,#9199,#9200,#9201,#9202,#9203,
#9204,#9205,#9206,#9207,#9208,#9209,#9210,#9211,#9212,#9213,#9214,#9215,
#9216),.UNSPECIFIED.,.F.,.F.,(4,3,3,3,3,3,4),(-71.548101301701,-71.0877887496107,
-70.1004583503106,-69.1131279510104,-68.1257975517103,-67.1384671524101,
-66.9247834919266),.UNSPECIFIED.);
#310=B_SPLINE_CURVE_WITH_KNOTS('',3,(#9219,#9220,#9221,#9222,#9223,#9224,
#9225,#9226,#9227),.UNSPECIFIED.,.F.,.F.,(4,1,1,1,1,1,4),(10.3761157273102,
11.2731783835768,12.2617453273021,13.2503122710274,14.2388792147526,15.2274461584779,
15.7079632679489),.UNSPECIFIED.);
#311=B_SPLINE_CURVE_WITH_KNOTS('',3,(#9545,#9546,#9547,#9548,#9549,#9550,
#9551,#9552,#9553,#9554,#9555,#9556,#9557,#9558,#9559,#9560,#9561,#9562,
#9563,#9564,#9565,#9566),.UNSPECIFIED.,.F.,.F.,(4,3,3,3,3,3,3,4),(63.9491534801641,
64.2568513421422,65.2454182858675,66.2339852295928,67.222552173318,68.2111191170433,
69.1996860607685,69.4794631267919),.UNSPECIFIED.);
#312=B_SPLINE_CURVE_WITH_KNOTS('',3,(#9567,#9568,#9569,#9570,#9571,#9572,
#9573,#9574,#9575,#9576,#9577,#9578,#9579,#9580,#9581,#9582,#9583,#9584,
#9585,#9586,#9587,#9588,#9589,#9590,#9591,#9592,#9593,#9594,#9595,#9596,
#9597,#9598,#9599,#9600,#9601,#9602,#9603,#9604,#9605,#9606,#9607,#9608,
#9609,#9610,#9611,#9612,#9613,#9614,#9615,#9616,#9617,#9618,#9619,#9620,
#9621,#9622,#9623,#9624,#9625,#9626,#9627,#9628,#9629,#9630,#9631,#9632,
#9633,#9634,#9635,#9636,#9637,#9638,#9639,#9640,#9641,#9642,#9643,#9644,
#9645,#9646,#9647,#9648,#9649,#9650,#9651,#9652,#9653,#9654),
 .UNSPECIFIED.,.F.,.F.,(4,3,3,3,3,3,3,3,3,3,3,3,3,3,3,3,3,3,3,3,3,3,3,3,
3,3,3,3,3,4),(-0.555272788399385,-0.533197712400843,-0.50841200558917,-0.492097097422296,
-0.487698425831477,-0.461722637175749,-0.438993822101987,-0.427671428401512,
-0.42202191869945,-0.395458071621424,-0.368431943977533,-0.346296987129563,
-0.329695769493585,-0.32517826205158,-0.321068892319616,-0.293156561268766,
-0.279892116585652,-0.25291117159626,-0.225403496298925,-0.221057334466692,
-0.216708298034074,-0.188764735094145,-0.160284152968102,-0.131561788206246,
-0.114355289595352,-0.109564750157472,-0.0800994390258527,-0.050557237845911,
-0.0215776241374192,0.),.UNSPECIFIED.);
#323=SHAPE_REPRESENTATION_RELATIONSHIP('SRR','None',#9867,#334);
#334=ADVANCED_BREP_SHAPE_REPRESENTATION('',(#356),#9776);
#345=STYLED_ITEM('',(#9930),#356);
#356=MANIFOLD_SOLID_BREP('Body1',#3850);
#408=FACE_BOUND('',#946,.T.);
#409=FACE_BOUND('',#949,.T.);
#492=PLANE('',#4289);
#493=PLANE('',#4290);
#494=PLANE('',#4291);
#495=PLANE('',#4292);
#496=PLANE('',#4293);
#497=PLANE('',#4294);
#498=PLANE('',#4295);
#499=PLANE('',#4296);
#500=PLANE('',#4300);
#501=PLANE('',#4301);
#662=FACE_OUTER_BOUND('',#911,.T.);
#663=FACE_OUTER_BOUND('',#912,.T.);
#664=FACE_OUTER_BOUND('',#913,.T.);
#665=FACE_OUTER_BOUND('',#914,.T.);
#666=FACE_OUTER_BOUND('',#915,.T.);
#667=FACE_OUTER_BOUND('',#916,.T.);
#668=FACE_OUTER_BOUND('',#917,.T.);
#669=FACE_OUTER_BOUND('',#918,.T.);
#670=FACE_OUTER_BOUND('',#919,.T.);
#671=FACE_OUTER_BOUND('',#920,.T.);
#672=FACE_OUTER_BOUND('',#921,.T.);
#673=FACE_OUTER_BOUND('',#922,.T.);
#674=FACE_OUTER_BOUND('',#923,.T.);
#675=FACE_OUTER_BOUND('',#924,.T.);
#676=FACE_OUTER_BOUND('',#925,.T.);
#677=FACE_OUTER_BOUND('',#926,.T.);
#678=FACE_OUTER_BOUND('',#927,.T.);
#679=FACE_OUTER_BOUND('',#928,.T.);
#680=FACE_OUTER_BOUND('',#929,.T.);
#681=FACE_OUTER_BOUND('',#930,.T.);
#682=FACE_OUTER_BOUND('',#931,.T.);
#683=FACE_OUTER_BOUND('',#932,.T.);
#684=FACE_OUTER_BOUND('',#933,.T.);
#685=FACE_OUTER_BOUND('',#934,.T.);
#686=FACE_OUTER_BOUND('',#935,.T.);
#687=FACE_OUTER_BOUND('',#936,.T.);
#688=FACE_OUTER_BOUND('',#937,.T.);
#689=FACE_OUTER_BOUND('',#938,.T.);
#690=FACE_OUTER_BOUND('',#939,.T.);
#691=FACE_OUTER_BOUND('',#940,.T.);
#692=FACE_OUTER_BOUND('',#941,.T.);
#693=FACE_OUTER_BOUND('',#942,.T.);
#694=FACE_OUTER_BOUND('',#943,.T.);
#695=FACE_OUTER_BOUND('',#944,.T.);
#696=FACE_OUTER_BOUND('',#945,.T.);
#697=FACE_OUTER_BOUND('',#947,.T.);
#698=FACE_OUTER_BOUND('',#948,.T.);
#699=FACE_OUTER_BOUND('',#950,.T.);
#911=EDGE_LOOP('',(#3337,#3338,#3339,#3340));
#912=EDGE_LOOP('',(#3341,#3342,#3343,#3344));
#913=EDGE_LOOP('',(#3345,#3346,#3347,#3348));
#914=EDGE_LOOP('',(#3349,#3350,#3351,#3352));
#915=EDGE_LOOP('',(#3353,#3354,#3355,#3356));
#916=EDGE_LOOP('',(#3357,#3358,#3359,#3360));
#917=EDGE_LOOP('',(#3361,#3362,#3363,#3364));
#918=EDGE_LOOP('',(#3365,#3366,#3367,#3368));
#919=EDGE_LOOP('',(#3369,#3370,#3371,#3372));
#920=EDGE_LOOP('',(#3373,#3374,#3375,#3376));
#921=EDGE_LOOP('',(#3377,#3378,#3379,#3380));
#922=EDGE_LOOP('',(#3381,#3382,#3383,#3384));
#923=EDGE_LOOP('',(#3385,#3386,#3387,#3388));
#924=EDGE_LOOP('',(#3389,#3390,#3391,#3392));
#925=EDGE_LOOP('',(#3393,#3394,#3395,#3396));
#926=EDGE_LOOP('',(#3397,#3398,#3399,#3400));
#927=EDGE_LOOP('',(#3401,#3402,#3403,#3404));
#928=EDGE_LOOP('',(#3405,#3406,#3407,#3408));
#929=EDGE_LOOP('',(#3409,#3410,#3411,#3412));
#930=EDGE_LOOP('',(#3413,#3414,#3415,#3416));
#931=EDGE_LOOP('',(#3417,#3418,#3419,#3420));
#932=EDGE_LOOP('',(#3421,#3422,#3423,#3424));
#933=EDGE_LOOP('',(#3425,#3426,#3427,#3428,#3429,#3430,#3431,#3432));
#934=EDGE_LOOP('',(#3433,#3434,#3435,#3436,#3437,#3438,#3439,#3440,#3441,
#3442,#3443,#3444,#3445,#3446,#3447,#3448,#3449,#3450,#3451,#3452,#3453,
#3454,#3455,#3456,#3457,#3458));
#935=EDGE_LOOP('',(#3459,#3460,#3461,#3462));
#936=EDGE_LOOP('',(#3463,#3464,#3465,#3466,#3467,#3468,#3469,#3470,#3471,
#3472,#3473,#3474,#3475,#3476,#3477,#3478,#3479,#3480,#3481,#3482,#3483,
#3484,#3485,#3486,#3487,#3488,#3489));
#937=EDGE_LOOP('',(#3490,#3491,#3492,#3493));
#938=EDGE_LOOP('',(#3494,#3495,#3496,#3497));
#939=EDGE_LOOP('',(#3498,#3499,#3500,#3501));
#940=EDGE_LOOP('',(#3502,#3503,#3504,#3505));
#941=EDGE_LOOP('',(#3506,#3507,#3508,#3509));
#942=EDGE_LOOP('',(#3510,#3511,#3512,#3513));
#943=EDGE_LOOP('',(#3514,#3515,#3516,#3517));
#944=EDGE_LOOP('',(#3518,#3519,#3520,#3521,#3522,#3523));
#945=EDGE_LOOP('',(#3524));
#946=EDGE_LOOP('',(#3525,#3526,#3527,#3528));
#947=EDGE_LOOP('',(#3529,#3530,#3531,#3532));
#948=EDGE_LOOP('',(#3533));
#949=EDGE_LOOP('',(#3534,#3535,#3536,#3537,#3538,#3539));
#950=EDGE_LOOP('',(#3540));
#1202=LINE('',#7685,#1495);
#1203=LINE('',#7709,#1496);
#1204=LINE('',#7757,#1497);
#1205=LINE('',#7805,#1498);
#1206=LINE('',#7859,#1499);
#1207=LINE('',#7907,#1500);
#1208=LINE('',#7955,#1501);
#1209=LINE('',#8009,#1502);
#1210=LINE('',#8057,#1503);
#1211=LINE('',#8108,#1504);
#1212=LINE('',#8159,#1505);
#1213=LINE('',#8207,#1506);
#1214=LINE('',#8232,#1507);
#1215=LINE('',#8257,#1508);
#1216=LINE('',#8281,#1509);
#1217=LINE('',#8307,#1510);
#1218=LINE('',#8331,#1511);
#1219=LINE('',#8356,#1512);
#1220=LINE('',#8381,#1513);
#1221=LINE('',#8405,#1514);
#1222=LINE('',#8430,#1515);
#1223=LINE('',#8455,#1516);
#1224=LINE('',#8791,#1517);
#1225=LINE('',#9659,#1518);
#1226=LINE('',#9661,#1519);
#1227=LINE('',#9663,#1520);
#1228=LINE('',#9664,#1521);
#1229=LINE('',#9667,#1522);
#1230=LINE('',#9669,#1523);
#1231=LINE('',#9670,#1524);
#1232=LINE('',#9673,#1525);
#1233=LINE('',#9675,#1526);
#1234=LINE('',#9676,#1527);
#1235=LINE('',#9679,#1528);
#1236=LINE('',#9681,#1529);
#1237=LINE('',#9682,#1530);
#1238=LINE('',#9685,#1531);
#1239=LINE('',#9687,#1532);
#1240=LINE('',#9688,#1533);
#1241=LINE('',#9690,#1534);
#1242=LINE('',#9691,#1535);
#1243=LINE('',#9698,#1536);
#1495=VECTOR('',#5177,3.);
#1496=VECTOR('',#5182,3.);
#1497=VECTOR('',#5185,3.);
#1498=VECTOR('',#5188,3.);
#1499=VECTOR('',#5191,3.);
#1500=VECTOR('',#5194,3.);
#1501=VECTOR('',#5197,3.);
#1502=VECTOR('',#5200,3.);
#1503=VECTOR('',#5203,3.);
#1504=VECTOR('',#5206,3.);
#1505=VECTOR('',#5209,3.);
#1506=VECTOR('',#5212,2.37175);
#1507=VECTOR('',#5217,2.37175);
#1508=VECTOR('',#5220,2.37175);
#1509=VECTOR('',#5223,2.37175);
#1510=VECTOR('',#5226,2.37175);
#1511=VECTOR('',#5229,2.37175);
#1512=VECTOR('',#5232,2.37175);
#1513=VECTOR('',#5235,2.37175);
#1514=VECTOR('',#5238,2.37175);
#1515=VECTOR('',#5241,2.37175);
#1516=VECTOR('',#5244,2.37175);
#1517=VECTOR('',#5249,2.5);
#1518=VECTOR('',#5260,10.);
#1519=VECTOR('',#5261,10.);
#1520=VECTOR('',#5262,10.);
#1521=VECTOR('',#5263,10.);
#1522=VECTOR('',#5266,10.);
#1523=VECTOR('',#5267,10.);
#1524=VECTOR('',#5268,10.);
#1525=VECTOR('',#5271,10.);
#1526=VECTOR('',#5272,10.);
#1527=VECTOR('',#5273,10.);
#1528=VECTOR('',#5276,10.);
#1529=VECTOR('',#5277,10.);
#1530=VECTOR('',#5278,10.);
#1531=VECTOR('',#5281,10.);
#1532=VECTOR('',#5282,10.);
#1533=VECTOR('',#5283,10.);
#1534=VECTOR('',#5286,10.);
#1535=VECTOR('',#5287,10.);
#1536=VECTOR('',#5296,5.);
#1653=CIRCLE('',#4260,2.942);
#1654=CIRCLE('',#4272,2.37175);
#1655=CIRCLE('',#4284,2.942);
#1656=CIRCLE('',#4285,2.);
#1657=CIRCLE('',#4287,2.37175);
#1658=CIRCLE('',#4297,5.);
#1659=CIRCLE('',#4299,5.);
#1934=VERTEX_POINT('',#7683);
#1935=VERTEX_POINT('',#7684);
#1936=VERTEX_POINT('',#7686);
#1937=VERTEX_POINT('',#7697);
#1938=VERTEX_POINT('',#7707);
#1939=VERTEX_POINT('',#7708);
#1940=VERTEX_POINT('',#7755);
#1941=VERTEX_POINT('',#7756);
#1942=VERTEX_POINT('',#7803);
#1943=VERTEX_POINT('',#7804);
#1944=VERTEX_POINT('',#7857);
#1945=VERTEX_POINT('',#7858);
#1946=VERTEX_POINT('',#7905);
#1947=VERTEX_POINT('',#7906);
#1948=VERTEX_POINT('',#7953);
#1949=VERTEX_POINT('',#7954);
#1950=VERTEX_POINT('',#8007);
#1951=VERTEX_POINT('',#8008);
#1952=VERTEX_POINT('',#8055);
#1953=VERTEX_POINT('',#8056);
#1954=VERTEX_POINT('',#8106);
#1955=VERTEX_POINT('',#8107);
#1956=VERTEX_POINT('',#8157);
#1957=VERTEX_POINT('',#8158);
#1958=VERTEX_POINT('',#8205);
#1959=VERTEX_POINT('',#8206);
#1960=VERTEX_POINT('',#8208);
#1961=VERTEX_POINT('',#8219);
#1962=VERTEX_POINT('',#8230);
#1963=VERTEX_POINT('',#8231);
#1964=VERTEX_POINT('',#8255);
#1965=VERTEX_POINT('',#8256);
#1966=VERTEX_POINT('',#8279);
#1967=VERTEX_POINT('',#8280);
#1968=VERTEX_POINT('',#8305);
#1969=VERTEX_POINT('',#8306);
#1970=VERTEX_POINT('',#8329);
#1971=VERTEX_POINT('',#8330);
#1972=VERTEX_POINT('',#8354);
#1973=VERTEX_POINT('',#8355);
#1974=VERTEX_POINT('',#8379);
#1975=VERTEX_POINT('',#8380);
#1976=VERTEX_POINT('',#8403);
#1977=VERTEX_POINT('',#8404);
#1978=VERTEX_POINT('',#8428);
#1979=VERTEX_POINT('',#8429);
#1980=VERTEX_POINT('',#8453);
#1981=VERTEX_POINT('',#8454);
#1982=VERTEX_POINT('',#8477);
#1983=VERTEX_POINT('',#8695);
#1984=VERTEX_POINT('',#8757);
#1985=VERTEX_POINT('',#8790);
#1986=VERTEX_POINT('',#9101);
#1987=VERTEX_POINT('',#9218);
#1988=VERTEX_POINT('',#9657);
#1989=VERTEX_POINT('',#9658);
#1990=VERTEX_POINT('',#9660);
#1991=VERTEX_POINT('',#9662);
#1992=VERTEX_POINT('',#9666);
#1993=VERTEX_POINT('',#9668);
#1994=VERTEX_POINT('',#9672);
#1995=VERTEX_POINT('',#9674);
#1996=VERTEX_POINT('',#9678);
#1997=VERTEX_POINT('',#9680);
#1998=VERTEX_POINT('',#9684);
#1999=VERTEX_POINT('',#9686);
#2000=VERTEX_POINT('',#9694);
#2001=VERTEX_POINT('',#9697);
#2413=EDGE_CURVE('',#1934,#1935,#1202,.T.);
#2414=EDGE_CURVE('',#1934,#1936,#260,.T.);
#2415=EDGE_CURVE('',#1936,#1937,#1653,.F.);
#2416=EDGE_CURVE('',#1937,#1935,#261,.T.);
#2417=EDGE_CURVE('',#1938,#1939,#1203,.T.);
#2418=EDGE_CURVE('',#1938,#1934,#262,.T.);
#2419=EDGE_CURVE('',#1935,#1939,#263,.T.);
#2420=EDGE_CURVE('',#1940,#1941,#1204,.T.);
#2421=EDGE_CURVE('',#1940,#1938,#264,.T.);
#2422=EDGE_CURVE('',#1939,#1941,#265,.T.);
#2423=EDGE_CURVE('',#1942,#1943,#1205,.T.);
#2424=EDGE_CURVE('',#1942,#1940,#266,.T.);
#2425=EDGE_CURVE('',#1941,#1943,#267,.T.);
#2426=EDGE_CURVE('',#1944,#1945,#1206,.T.);
#2427=EDGE_CURVE('',#1944,#1942,#268,.T.);
#2428=EDGE_CURVE('',#1943,#1945,#269,.T.);
#2429=EDGE_CURVE('',#1946,#1947,#1207,.T.);
#2430=EDGE_CURVE('',#1946,#1944,#270,.T.);
#2431=EDGE_CURVE('',#1945,#1947,#271,.T.);
#2432=EDGE_CURVE('',#1948,#1949,#1208,.T.);
#2433=EDGE_CURVE('',#1948,#1946,#272,.T.);
#2434=EDGE_CURVE('',#1947,#1949,#273,.T.);
#2435=EDGE_CURVE('',#1950,#1951,#1209,.T.);
#2436=EDGE_CURVE('',#1950,#1948,#274,.T.);
#2437=EDGE_CURVE('',#1949,#1951,#275,.T.);
#2438=EDGE_CURVE('',#1952,#1953,#1210,.T.);
#2439=EDGE_CURVE('',#1952,#1950,#276,.T.);
#2440=EDGE_CURVE('',#1951,#1953,#277,.T.);
#2441=EDGE_CURVE('',#1954,#1955,#1211,.T.);
#2442=EDGE_CURVE('',#1954,#1952,#278,.T.);
#2443=EDGE_CURVE('',#1953,#1955,#279,.T.);
#2444=EDGE_CURVE('',#1956,#1957,#1212,.T.);
#2445=EDGE_CURVE('',#1956,#1954,#280,.T.);
#2446=EDGE_CURVE('',#1955,#1957,#281,.T.);
#2447=EDGE_CURVE('',#1958,#1959,#1213,.T.);
#2448=EDGE_CURVE('',#1958,#1960,#282,.T.);
#2449=EDGE_CURVE('',#1960,#1961,#1654,.T.);
#2450=EDGE_CURVE('',#1959,#1961,#283,.T.);
#2451=EDGE_CURVE('',#1962,#1963,#1214,.T.);
#2452=EDGE_CURVE('',#1962,#1958,#284,.T.);
#2453=EDGE_CURVE('',#1963,#1959,#285,.T.);
#2454=EDGE_CURVE('',#1964,#1965,#1215,.T.);
#2455=EDGE_CURVE('',#1964,#1962,#286,.T.);
#2456=EDGE_CURVE('',#1965,#1963,#287,.T.);
#2457=EDGE_CURVE('',#1966,#1967,#1216,.T.);
#2458=EDGE_CURVE('',#1966,#1964,#288,.T.);
#2459=EDGE_CURVE('',#1967,#1965,#289,.T.);
#2460=EDGE_CURVE('',#1968,#1969,#1217,.T.);
#2461=EDGE_CURVE('',#1968,#1966,#290,.T.);
#2462=EDGE_CURVE('',#1969,#1967,#291,.T.);
#2463=EDGE_CURVE('',#1970,#1971,#1218,.T.);
#2464=EDGE_CURVE('',#1970,#1968,#292,.T.);
#2465=EDGE_CURVE('',#1971,#1969,#293,.T.);
#2466=EDGE_CURVE('',#1972,#1973,#1219,.T.);
#2467=EDGE_CURVE('',#1972,#1970,#294,.T.);
#2468=EDGE_CURVE('',#1973,#1971,#295,.T.);
#2469=EDGE_CURVE('',#1974,#1975,#1220,.T.);
#2470=EDGE_CURVE('',#1974,#1972,#296,.T.);
#2471=EDGE_CURVE('',#1975,#1973,#297,.T.);
#2472=EDGE_CURVE('',#1976,#1977,#1221,.T.);
#2473=EDGE_CURVE('',#1976,#1974,#298,.T.);
#2474=EDGE_CURVE('',#1977,#1975,#299,.T.);
#2475=EDGE_CURVE('',#1978,#1979,#1222,.T.);
#2476=EDGE_CURVE('',#1978,#1976,#300,.T.);
#2477=EDGE_CURVE('',#1979,#1977,#301,.T.);
#2478=EDGE_CURVE('',#1980,#1981,#1223,.T.);
#2479=EDGE_CURVE('',#1980,#1978,#302,.T.);
#2480=EDGE_CURVE('',#1981,#1979,#303,.T.);
#2481=EDGE_CURVE('',#1961,#1982,#304,.T.);
#2482=EDGE_CURVE('',#1983,#1960,#305,.T.);
#2483=EDGE_CURVE('',#1984,#1983,#1655,.T.);
#2484=EDGE_CURVE('',#1982,#1984,#306,.T.);
#2485=EDGE_CURVE('',#1982,#1985,#1224,.T.);
#2486=EDGE_CURVE('',#1985,#1985,#1656,.T.);
#2487=EDGE_CURVE('',#1986,#1980,#307,.T.);
#2488=EDGE_CURVE('',#1936,#1986,#308,.T.);
#2489=EDGE_CURVE('',#1983,#1956,#309,.T.);
#2490=EDGE_CURVE('',#1987,#1981,#310,.T.);
#2491=EDGE_CURVE('',#1986,#1987,#1657,.T.);
#2492=EDGE_CURVE('',#1957,#1984,#311,.T.);
#2493=EDGE_CURVE('',#1987,#1937,#312,.T.);
#2494=EDGE_CURVE('',#1988,#1989,#1225,.T.);
#2495=EDGE_CURVE('',#1988,#1990,#1226,.T.);
#2496=EDGE_CURVE('',#1990,#1991,#1227,.T.);
#2497=EDGE_CURVE('',#1989,#1991,#1228,.T.);
#2498=EDGE_CURVE('',#1992,#1988,#1229,.T.);
#2499=EDGE_CURVE('',#1992,#1993,#1230,.T.);
#2500=EDGE_CURVE('',#1993,#1990,#1231,.T.);
#2501=EDGE_CURVE('',#1994,#1992,#1232,.T.);
#2502=EDGE_CURVE('',#1994,#1995,#1233,.T.);
#2503=EDGE_CURVE('',#1995,#1993,#1234,.T.);
#2504=EDGE_CURVE('',#1996,#1994,#1235,.T.);
#2505=EDGE_CURVE('',#1996,#1997,#1236,.T.);
#2506=EDGE_CURVE('',#1997,#1995,#1237,.T.);
#2507=EDGE_CURVE('',#1998,#1996,#1238,.T.);
#2508=EDGE_CURVE('',#1998,#1999,#1239,.T.);
#2509=EDGE_CURVE('',#1999,#1997,#1240,.T.);
#2510=EDGE_CURVE('',#1989,#1998,#1241,.T.);
#2511=EDGE_CURVE('',#1991,#1999,#1242,.T.);
#2512=EDGE_CURVE('',#2000,#2000,#1658,.T.);
#2513=EDGE_CURVE('',#2000,#2001,#1243,.T.);
#2514=EDGE_CURVE('',#2001,#2001,#1659,.T.);
#3337=ORIENTED_EDGE('',*,*,#2413,.F.);
#3338=ORIENTED_EDGE('',*,*,#2414,.T.);
#3339=ORIENTED_EDGE('',*,*,#2415,.T.);
#3340=ORIENTED_EDGE('',*,*,#2416,.T.);
#3341=ORIENTED_EDGE('',*,*,#2417,.F.);
#3342=ORIENTED_EDGE('',*,*,#2418,.T.);
#3343=ORIENTED_EDGE('',*,*,#2413,.T.);
#3344=ORIENTED_EDGE('',*,*,#2419,.T.);
#3345=ORIENTED_EDGE('',*,*,#2420,.F.);
#3346=ORIENTED_EDGE('',*,*,#2421,.T.);
#3347=ORIENTED_EDGE('',*,*,#2417,.T.);
#3348=ORIENTED_EDGE('',*,*,#2422,.T.);
#3349=ORIENTED_EDGE('',*,*,#2423,.F.);
#3350=ORIENTED_EDGE('',*,*,#2424,.T.);
#3351=ORIENTED_EDGE('',*,*,#2420,.T.);
#3352=ORIENTED_EDGE('',*,*,#2425,.T.);
#3353=ORIENTED_EDGE('',*,*,#2426,.F.);
#3354=ORIENTED_EDGE('',*,*,#2427,.T.);
#3355=ORIENTED_EDGE('',*,*,#2423,.T.);
#3356=ORIENTED_EDGE('',*,*,#2428,.T.);
#3357=ORIENTED_EDGE('',*,*,#2429,.F.);
#3358=ORIENTED_EDGE('',*,*,#2430,.T.);
#3359=ORIENTED_EDGE('',*,*,#2426,.T.);
#3360=ORIENTED_EDGE('',*,*,#2431,.T.);
#3361=ORIENTED_EDGE('',*,*,#2432,.F.);
#3362=ORIENTED_EDGE('',*,*,#2433,.T.);
#3363=ORIENTED_EDGE('',*,*,#2429,.T.);
#3364=ORIENTED_EDGE('',*,*,#2434,.T.);
#3365=ORIENTED_EDGE('',*,*,#2435,.F.);
#3366=ORIENTED_EDGE('',*,*,#2436,.T.);
#3367=ORIENTED_EDGE('',*,*,#2432,.T.);
#3368=ORIENTED_EDGE('',*,*,#2437,.T.);
#3369=ORIENTED_EDGE('',*,*,#2438,.F.);
#3370=ORIENTED_EDGE('',*,*,#2439,.T.);
#3371=ORIENTED_EDGE('',*,*,#2435,.T.);
#3372=ORIENTED_EDGE('',*,*,#2440,.T.);
#3373=ORIENTED_EDGE('',*,*,#2441,.F.);
#3374=ORIENTED_EDGE('',*,*,#2442,.T.);
#3375=ORIENTED_EDGE('',*,*,#2438,.T.);
#3376=ORIENTED_EDGE('',*,*,#2443,.T.);
#3377=ORIENTED_EDGE('',*,*,#2444,.F.);
#3378=ORIENTED_EDGE('',*,*,#2445,.T.);
#3379=ORIENTED_EDGE('',*,*,#2441,.T.);
#3380=ORIENTED_EDGE('',*,*,#2446,.T.);
#3381=ORIENTED_EDGE('',*,*,#2447,.F.);
#3382=ORIENTED_EDGE('',*,*,#2448,.T.);
#3383=ORIENTED_EDGE('',*,*,#2449,.T.);
#3384=ORIENTED_EDGE('',*,*,#2450,.F.);
#3385=ORIENTED_EDGE('',*,*,#2451,.F.);
#3386=ORIENTED_EDGE('',*,*,#2452,.T.);
#3387=ORIENTED_EDGE('',*,*,#2447,.T.);
#3388=ORIENTED_EDGE('',*,*,#2453,.F.);
#3389=ORIENTED_EDGE('',*,*,#2454,.F.);
#3390=ORIENTED_EDGE('',*,*,#2455,.T.);
#3391=ORIENTED_EDGE('',*,*,#2451,.T.);
#3392=ORIENTED_EDGE('',*,*,#2456,.F.);
#3393=ORIENTED_EDGE('',*,*,#2457,.F.);
#3394=ORIENTED_EDGE('',*,*,#2458,.T.);
#3395=ORIENTED_EDGE('',*,*,#2454,.T.);
#3396=ORIENTED_EDGE('',*,*,#2459,.F.);
#3397=ORIENTED_EDGE('',*,*,#2460,.F.);
#3398=ORIENTED_EDGE('',*,*,#2461,.T.);
#3399=ORIENTED_EDGE('',*,*,#2457,.T.);
#3400=ORIENTED_EDGE('',*,*,#2462,.F.);
#3401=ORIENTED_EDGE('',*,*,#2463,.F.);
#3402=ORIENTED_EDGE('',*,*,#2464,.T.);
#3403=ORIENTED_EDGE('',*,*,#2460,.T.);
#3404=ORIENTED_EDGE('',*,*,#2465,.F.);
#3405=ORIENTED_EDGE('',*,*,#2466,.F.);
#3406=ORIENTED_EDGE('',*,*,#2467,.T.);
#3407=ORIENTED_EDGE('',*,*,#2463,.T.);
#3408=ORIENTED_EDGE('',*,*,#2468,.F.);
#3409=ORIENTED_EDGE('',*,*,#2469,.F.);
#3410=ORIENTED_EDGE('',*,*,#2470,.T.);
#3411=ORIENTED_EDGE('',*,*,#2466,.T.);
#3412=ORIENTED_EDGE('',*,*,#2471,.F.);
#3413=ORIENTED_EDGE('',*,*,#2472,.F.);
#3414=ORIENTED_EDGE('',*,*,#2473,.T.);
#3415=ORIENTED_EDGE('',*,*,#2469,.T.);
#3416=ORIENTED_EDGE('',*,*,#2474,.F.);
#3417=ORIENTED_EDGE('',*,*,#2475,.F.);
#3418=ORIENTED_EDGE('',*,*,#2476,.T.);
#3419=ORIENTED_EDGE('',*,*,#2472,.T.);
#3420=ORIENTED_EDGE('',*,*,#2477,.F.);
#3421=ORIENTED_EDGE('',*,*,#2478,.F.);
#3422=ORIENTED_EDGE('',*,*,#2479,.T.);
#3423=ORIENTED_EDGE('',*,*,#2475,.T.);
#3424=ORIENTED_EDGE('',*,*,#2480,.F.);
#3425=ORIENTED_EDGE('',*,*,#2481,.F.);
#3426=ORIENTED_EDGE('',*,*,#2449,.F.);
#3427=ORIENTED_EDGE('',*,*,#2482,.F.);
#3428=ORIENTED_EDGE('',*,*,#2483,.F.);
#3429=ORIENTED_EDGE('',*,*,#2484,.F.);
#3430=ORIENTED_EDGE('',*,*,#2485,.T.);
#3431=ORIENTED_EDGE('',*,*,#2486,.F.);
#3432=ORIENTED_EDGE('',*,*,#2485,.F.);
#3433=ORIENTED_EDGE('',*,*,#2482,.T.);
#3434=ORIENTED_EDGE('',*,*,#2448,.F.);
#3435=ORIENTED_EDGE('',*,*,#2452,.F.);
#3436=ORIENTED_EDGE('',*,*,#2455,.F.);
#3437=ORIENTED_EDGE('',*,*,#2458,.F.);
#3438=ORIENTED_EDGE('',*,*,#2461,.F.);
#3439=ORIENTED_EDGE('',*,*,#2464,.F.);
#3440=ORIENTED_EDGE('',*,*,#2467,.F.);
#3441=ORIENTED_EDGE('',*,*,#2470,.F.);
#3442=ORIENTED_EDGE('',*,*,#2473,.F.);
#3443=ORIENTED_EDGE('',*,*,#2476,.F.);
#3444=ORIENTED_EDGE('',*,*,#2479,.F.);
#3445=ORIENTED_EDGE('',*,*,#2487,.F.);
#3446=ORIENTED_EDGE('',*,*,#2488,.F.);
#3447=ORIENTED_EDGE('',*,*,#2414,.F.);
#3448=ORIENTED_EDGE('',*,*,#2418,.F.);
#3449=ORIENTED_EDGE('',*,*,#2421,.F.);
#3450=ORIENTED_EDGE('',*,*,#2424,.F.);
#3451=ORIENTED_EDGE('',*,*,#2427,.F.);
#3452=ORIENTED_EDGE('',*,*,#2430,.F.);
#3453=ORIENTED_EDGE('',*,*,#2433,.F.);
#3454=ORIENTED_EDGE('',*,*,#2436,.F.);
#3455=ORIENTED_EDGE('',*,*,#2439,.F.);
#3456=ORIENTED_EDGE('',*,*,#2442,.F.);
#3457=ORIENTED_EDGE('',*,*,#2445,.F.);
#3458=ORIENTED_EDGE('',*,*,#2489,.F.);
#3459=ORIENTED_EDGE('',*,*,#2478,.T.);
#3460=ORIENTED_EDGE('',*,*,#2490,.F.);
#3461=ORIENTED_EDGE('',*,*,#2491,.F.);
#3462=ORIENTED_EDGE('',*,*,#2487,.T.);
#3463=ORIENTED_EDGE('',*,*,#2481,.T.);
#3464=ORIENTED_EDGE('',*,*,#2484,.T.);
#3465=ORIENTED_EDGE('',*,*,#2492,.F.);
#3466=ORIENTED_EDGE('',*,*,#2446,.F.);
#3467=ORIENTED_EDGE('',*,*,#2443,.F.);
#3468=ORIENTED_EDGE('',*,*,#2440,.F.);
#3469=ORIENTED_EDGE('',*,*,#2437,.F.);
#3470=ORIENTED_EDGE('',*,*,#2434,.F.);
#3471=ORIENTED_EDGE('',*,*,#2431,.F.);
#3472=ORIENTED_EDGE('',*,*,#2428,.F.);
#3473=ORIENTED_EDGE('',*,*,#2425,.F.);
#3474=ORIENTED_EDGE('',*,*,#2422,.F.);
#3475=ORIENTED_EDGE('',*,*,#2419,.F.);
#3476=ORIENTED_EDGE('',*,*,#2416,.F.);
#3477=ORIENTED_EDGE('',*,*,#2493,.F.);
#3478=ORIENTED_EDGE('',*,*,#2490,.T.);
#3479=ORIENTED_EDGE('',*,*,#2480,.T.);
#3480=ORIENTED_EDGE('',*,*,#2477,.T.);
#3481=ORIENTED_EDGE('',*,*,#2474,.T.);
#3482=ORIENTED_EDGE('',*,*,#2471,.T.);
#3483=ORIENTED_EDGE('',*,*,#2468,.T.);
#3484=ORIENTED_EDGE('',*,*,#2465,.T.);
#3485=ORIENTED_EDGE('',*,*,#2462,.T.);
#3486=ORIENTED_EDGE('',*,*,#2459,.T.);
#3487=ORIENTED_EDGE('',*,*,#2456,.T.);
#3488=ORIENTED_EDGE('',*,*,#2453,.T.);
#3489=ORIENTED_EDGE('',*,*,#2450,.T.);
#3490=ORIENTED_EDGE('',*,*,#2444,.T.);
#3491=ORIENTED_EDGE('',*,*,#2492,.T.);
#3492=ORIENTED_EDGE('',*,*,#2483,.T.);
#3493=ORIENTED_EDGE('',*,*,#2489,.T.);
#3494=ORIENTED_EDGE('',*,*,#2494,.F.);
#3495=ORIENTED_EDGE('',*,*,#2495,.T.);
#3496=ORIENTED_EDGE('',*,*,#2496,.T.);
#3497=ORIENTED_EDGE('',*,*,#2497,.F.);
#3498=ORIENTED_EDGE('',*,*,#2498,.F.);
#3499=ORIENTED_EDGE('',*,*,#2499,.T.);
#3500=ORIENTED_EDGE('',*,*,#2500,.T.);
#3501=ORIENTED_EDGE('',*,*,#2495,.F.);
#3502=ORIENTED_EDGE('',*,*,#2501,.F.);
#3503=ORIENTED_EDGE('',*,*,#2502,.T.);
#3504=ORIENTED_EDGE('',*,*,#2503,.T.);
#3505=ORIENTED_EDGE('',*,*,#2499,.F.);
#3506=ORIENTED_EDGE('',*,*,#2504,.F.);
#3507=ORIENTED_EDGE('',*,*,#2505,.T.);
#3508=ORIENTED_EDGE('',*,*,#2506,.T.);
#3509=ORIENTED_EDGE('',*,*,#2502,.F.);
#3510=ORIENTED_EDGE('',*,*,#2507,.F.);
#3511=ORIENTED_EDGE('',*,*,#2508,.T.);
#3512=ORIENTED_EDGE('',*,*,#2509,.T.);
#3513=ORIENTED_EDGE('',*,*,#2505,.F.);
#3514=ORIENTED_EDGE('',*,*,#2510,.F.);
#3515=ORIENTED_EDGE('',*,*,#2497,.T.);
#3516=ORIENTED_EDGE('',*,*,#2511,.T.);
#3517=ORIENTED_EDGE('',*,*,#2508,.F.);
#3518=ORIENTED_EDGE('',*,*,#2511,.F.);
#3519=ORIENTED_EDGE('',*,*,#2496,.F.);
#3520=ORIENTED_EDGE('',*,*,#2500,.F.);
#3521=ORIENTED_EDGE('',*,*,#2503,.F.);
#3522=ORIENTED_EDGE('',*,*,#2506,.F.);
#3523=ORIENTED_EDGE('',*,*,#2509,.F.);
#3524=ORIENTED_EDGE('',*,*,#2512,.T.);
#3525=ORIENTED_EDGE('',*,*,#2488,.T.);
#3526=ORIENTED_EDGE('',*,*,#2491,.T.);
#3527=ORIENTED_EDGE('',*,*,#2493,.T.);
#3528=ORIENTED_EDGE('',*,*,#2415,.F.);
#3529=ORIENTED_EDGE('',*,*,#2512,.F.);
#3530=ORIENTED_EDGE('',*,*,#2513,.T.);
#3531=ORIENTED_EDGE('',*,*,#2514,.T.);
#3532=ORIENTED_EDGE('',*,*,#2513,.F.);
#3533=ORIENTED_EDGE('',*,*,#2514,.F.);
#3534=ORIENTED_EDGE('',*,*,#2494,.T.);
#3535=ORIENTED_EDGE('',*,*,#2510,.T.);
#3536=ORIENTED_EDGE('',*,*,#2507,.T.);
#3537=ORIENTED_EDGE('',*,*,#2504,.T.);
#3538=ORIENTED_EDGE('',*,*,#2501,.T.);
#3539=ORIENTED_EDGE('',*,*,#2498,.T.);
#3540=ORIENTED_EDGE('',*,*,#2486,.T.);
#3617=CYLINDRICAL_SURFACE('',#4259,2.942);
#3618=CYLINDRICAL_SURFACE('',#4261,2.942);
#3619=CYLINDRICAL_SURFACE('',#4262,2.942);
#3620=CYLINDRICAL_SURFACE('',#4263,2.942);
#3621=CYLINDRICAL_SURFACE('',#4264,2.942);
#3622=CYLINDRICAL_SURFACE('',#4265,2.942);
#3623=CYLINDRICAL_SURFACE('',#4266,2.942);
#3624=CYLINDRICAL_SURFACE('',#4267,2.942);
#3625=CYLINDRICAL_SURFACE('',#4268,2.942);
#3626=CYLINDRICAL_SURFACE('',#4269,2.942);
#3627=CYLINDRICAL_SURFACE('',#4270,2.942);
#3628=CYLINDRICAL_SURFACE('',#4271,2.37175);
#3629=CYLINDRICAL_SURFACE('',#4273,2.37175);
#3630=CYLINDRICAL_SURFACE('',#4274,2.37175);
#3631=CYLINDRICAL_SURFACE('',#4275,2.37175);
#3632=CYLINDRICAL_SURFACE('',#4276,2.37175);
#3633=CYLINDRICAL_SURFACE('',#4277,2.37175);
#3634=CYLINDRICAL_SURFACE('',#4278,2.37175);
#3635=CYLINDRICAL_SURFACE('',#4279,2.37175);
#3636=CYLINDRICAL_SURFACE('',#4280,2.37175);
#3637=CYLINDRICAL_SURFACE('',#4281,2.37175);
#3638=CYLINDRICAL_SURFACE('',#4282,2.37175);
#3639=CYLINDRICAL_SURFACE('',#4286,2.37175);
#3640=CYLINDRICAL_SURFACE('',#4288,2.942);
#3641=CYLINDRICAL_SURFACE('',#4298,5.);
#3802=ADVANCED_FACE('',(#662),#3617,.T.);
#3803=ADVANCED_FACE('',(#663),#3618,.T.);
#3804=ADVANCED_FACE('',(#664),#3619,.T.);
#3805=ADVANCED_FACE('',(#665),#3620,.T.);
#3806=ADVANCED_FACE('',(#666),#3621,.T.);
#3807=ADVANCED_FACE('',(#667),#3622,.T.);
#3808=ADVANCED_FACE('',(#668),#3623,.T.);
#3809=ADVANCED_FACE('',(#669),#3624,.T.);
#3810=ADVANCED_FACE('',(#670),#3625,.T.);
#3811=ADVANCED_FACE('',(#671),#3626,.T.);
#3812=ADVANCED_FACE('',(#672),#3627,.T.);
#3813=ADVANCED_FACE('',(#673),#3628,.T.);
#3814=ADVANCED_FACE('',(#674),#3629,.T.);
#3815=ADVANCED_FACE('',(#675),#3630,.T.);
#3816=ADVANCED_FACE('',(#676),#3631,.T.);
#3817=ADVANCED_FACE('',(#677),#3632,.T.);
#3818=ADVANCED_FACE('',(#678),#3633,.T.);
#3819=ADVANCED_FACE('',(#679),#3634,.T.);
#3820=ADVANCED_FACE('',(#680),#3635,.T.);
#3821=ADVANCED_FACE('',(#681),#3636,.T.);
#3822=ADVANCED_FACE('',(#682),#3637,.T.);
#3823=ADVANCED_FACE('',(#683),#3638,.T.);
#3824=ADVANCED_FACE('',(#684),#211,.T.);
#3825=ADVANCED_FACE('',(#685),#214,.F.);
#3826=ADVANCED_FACE('',(#686),#3639,.T.);
#3827=ADVANCED_FACE('',(#687),#215,.F.);
#3828=ADVANCED_FACE('',(#688),#3640,.T.);
#3829=ADVANCED_FACE('',(#689),#492,.F.);
#3830=ADVANCED_FACE('',(#690),#493,.F.);
#3831=ADVANCED_FACE('',(#691),#494,.F.);
#3832=ADVANCED_FACE('',(#692),#495,.F.);
#3833=ADVANCED_FACE('',(#693),#496,.F.);
#3834=ADVANCED_FACE('',(#694),#497,.F.);
#3835=ADVANCED_FACE('',(#695),#498,.F.);
#3836=ADVANCED_FACE('',(#696,#408),#499,.T.);
#3837=ADVANCED_FACE('',(#697),#3641,.T.);
#3838=ADVANCED_FACE('',(#698,#409),#500,.F.);
#3839=ADVANCED_FACE('',(#699),#501,.T.);
#3850=CLOSED_SHELL('',(#3802,#3803,#3804,#3805,#3806,#3807,#3808,#3809,
#3810,#3811,#3812,#3813,#3814,#3815,#3816,#3817,#3818,#3819,#3820,#3821,
#3822,#3823,#3824,#3825,#3826,#3827,#3828,#3829,#3830,#3831,#3832,#3833,
#3834,#3835,#3836,#3837,#3838,#3839));
#4258=AXIS2_PLACEMENT_3D('',#7681,#5173,#5174);
#4259=AXIS2_PLACEMENT_3D('',#7682,#5175,#5176);
#4260=AXIS2_PLACEMENT_3D('',#7698,#5178,#5179);
#4261=AXIS2_PLACEMENT_3D('',#7706,#5180,#5181);
#4262=AXIS2_PLACEMENT_3D('',#7754,#5183,#5184);
#4263=AXIS2_PLACEMENT_3D('',#7802,#5186,#5187);
#4264=AXIS2_PLACEMENT_3D('',#7856,#5189,#5190);
#4265=AXIS2_PLACEMENT_3D('',#7904,#5192,#5193);
#4266=AXIS2_PLACEMENT_3D('',#7952,#5195,#5196);
#4267=AXIS2_PLACEMENT_3D('',#8006,#5198,#5199);
#4268=AXIS2_PLACEMENT_3D('',#8054,#5201,#5202);
#4269=AXIS2_PLACEMENT_3D('',#8105,#5204,#5205);
#4270=AXIS2_PLACEMENT_3D('',#8156,#5207,#5208);
#4271=AXIS2_PLACEMENT_3D('',#8204,#5210,#5211);
#4272=AXIS2_PLACEMENT_3D('',#8220,#5213,#5214);
#4273=AXIS2_PLACEMENT_3D('',#8229,#5215,#5216);
#4274=AXIS2_PLACEMENT_3D('',#8254,#5218,#5219);
#4275=AXIS2_PLACEMENT_3D('',#8278,#5221,#5222);
#4276=AXIS2_PLACEMENT_3D('',#8304,#5224,#5225);
#4277=AXIS2_PLACEMENT_3D('',#8328,#5227,#5228);
#4278=AXIS2_PLACEMENT_3D('',#8353,#5230,#5231);
#4279=AXIS2_PLACEMENT_3D('',#8378,#5233,#5234);
#4280=AXIS2_PLACEMENT_3D('',#8402,#5236,#5237);
#4281=AXIS2_PLACEMENT_3D('',#8427,#5239,#5240);
#4282=AXIS2_PLACEMENT_3D('',#8452,#5242,#5243);
#4283=AXIS2_PLACEMENT_3D('',#8476,#5245,#5246);
#4284=AXIS2_PLACEMENT_3D('',#8758,#5247,#5248);
#4285=AXIS2_PLACEMENT_3D('',#8792,#5250,#5251);
#4286=AXIS2_PLACEMENT_3D('',#9217,#5252,#5253);
#4287=AXIS2_PLACEMENT_3D('',#9228,#5254,#5255);
#4288=AXIS2_PLACEMENT_3D('',#9655,#5256,#5257);
#4289=AXIS2_PLACEMENT_3D('',#9656,#5258,#5259);
#4290=AXIS2_PLACEMENT_3D('',#9665,#5264,#5265);
#4291=AXIS2_PLACEMENT_3D('',#9671,#5269,#5270);
#4292=AXIS2_PLACEMENT_3D('',#9677,#5274,#5275);
#4293=AXIS2_PLACEMENT_3D('',#9683,#5279,#5280);
#4294=AXIS2_PLACEMENT_3D('',#9689,#5284,#5285);
#4295=AXIS2_PLACEMENT_3D('',#9692,#5288,#5289);
#4296=AXIS2_PLACEMENT_3D('',#9693,#5290,#5291);
#4297=AXIS2_PLACEMENT_3D('',#9695,#5292,#5293);
#4298=AXIS2_PLACEMENT_3D('',#9696,#5294,#5295);
#4299=AXIS2_PLACEMENT_3D('',#9699,#5297,#5298);
#4300=AXIS2_PLACEMENT_3D('',#9700,#5299,#5300);
#4301=AXIS2_PLACEMENT_3D('',#9701,#5301,#5302);
#5173=DIRECTION('axis',(0.,0.,1.));
#5174=DIRECTION('refdir',(1.,0.,0.));
#5175=DIRECTION('center_axis',(0.,0.,1.));
#5176=DIRECTION('ref_axis',(1.,0.,0.));
#5177=DIRECTION('',(0.,0.,-1.));
#5178=DIRECTION('center_axis',(0.,0.,-1.));
#5179=DIRECTION('ref_axis',(1.,0.,0.));
#5180=DIRECTION('center_axis',(0.,0.,1.));
#5181=DIRECTION('ref_axis',(1.,0.,0.));
#5182=DIRECTION('',(0.,0.,-1.));
#5183=DIRECTION('center_axis',(0.,0.,1.));
#5184=DIRECTION('ref_axis',(1.,0.,0.));
#5185=DIRECTION('',(0.,0.,-1.));
#5186=DIRECTION('center_axis',(0.,0.,1.));
#5187=DIRECTION('ref_axis',(1.,0.,0.));
#5188=DIRECTION('',(0.,0.,-1.));
#5189=DIRECTION('center_axis',(0.,0.,1.));
#5190=DIRECTION('ref_axis',(1.,0.,0.));
#5191=DIRECTION('',(0.,0.,-1.));
#5192=DIRECTION('center_axis',(0.,0.,1.));
#5193=DIRECTION('ref_axis',(1.,0.,0.));
#5194=DIRECTION('',(0.,0.,-1.));
#5195=DIRECTION('center_axis',(0.,0.,1.));
#5196=DIRECTION('ref_axis',(1.,0.,0.));
#5197=DIRECTION('',(0.,0.,-1.));
#5198=DIRECTION('center_axis',(0.,0.,1.));
#5199=DIRECTION('ref_axis',(1.,0.,0.));
#5200=DIRECTION('',(0.,0.,-1.));
#5201=DIRECTION('center_axis',(0.,0.,1.));
#5202=DIRECTION('ref_axis',(1.,0.,0.));
#5203=DIRECTION('',(0.,0.,-1.));
#5204=DIRECTION('center_axis',(0.,0.,1.));
#5205=DIRECTION('ref_axis',(1.,0.,0.));
#5206=DIRECTION('',(0.,0.,-1.));
#5207=DIRECTION('center_axis',(0.,0.,1.));
#5208=DIRECTION('ref_axis',(1.,0.,0.));
#5209=DIRECTION('',(0.,0.,-1.));
#5210=DIRECTION('center_axis',(0.,0.,1.));
#5211=DIRECTION('ref_axis',(0.997344302588954,-0.0728309144069492,0.));
#5212=DIRECTION('',(0.,0.,1.));
#5213=DIRECTION('center_axis',(0.,0.,-1.));
#5214=DIRECTION('ref_axis',(1.,7.52212518638754E-14,0.));
#5215=DIRECTION('center_axis',(0.,0.,1.));
#5216=DIRECTION('ref_axis',(1.,7.52212518638754E-14,0.));
#5217=DIRECTION('',(0.,0.,1.));
#5218=DIRECTION('center_axis',(0.,0.,1.));
#5219=DIRECTION('ref_axis',(1.,7.52212518638754E-14,0.));
#5220=DIRECTION('',(0.,0.,1.));
#5221=DIRECTION('center_axis',(0.,0.,1.));
#5222=DIRECTION('ref_axis',(1.,7.52212518638754E-14,0.));
#5223=DIRECTION('',(0.,0.,1.));
#5224=DIRECTION('center_axis',(0.,0.,1.));
#5225=DIRECTION('ref_axis',(1.,7.52212518638754E-14,0.));
#5226=DIRECTION('',(0.,0.,1.));
#5227=DIRECTION('center_axis',(0.,0.,1.));
#5228=DIRECTION('ref_axis',(1.,7.52212518638754E-14,0.));
#5229=DIRECTION('',(0.,0.,1.));
#5230=DIRECTION('center_axis',(0.,0.,1.));
#5231=DIRECTION('ref_axis',(1.,7.52212518638754E-14,0.));
#5232=DIRECTION('',(0.,0.,1.));
#5233=DIRECTION('center_axis',(0.,0.,1.));
#5234=DIRECTION('ref_axis',(1.,7.52212518638754E-14,0.));
#5235=DIRECTION('',(0.,0.,1.));
#5236=DIRECTION('center_axis',(0.,0.,1.));
#5237=DIRECTION('ref_axis',(1.,7.52212518638754E-14,0.));
#5238=DIRECTION('',(0.,0.,1.));
#5239=DIRECTION('center_axis',(0.,0.,1.));
#5240=DIRECTION('ref_axis',(1.,7.52212518638754E-14,0.));
#5241=DIRECTION('',(0.,0.,1.));
#5242=DIRECTION('center_axis',(0.,0.,1.));
#5243=DIRECTION('ref_axis',(1.,7.52212518638754E-14,0.));
#5244=DIRECTION('',(0.,0.,1.));
#5245=DIRECTION('center_axis',(0.,0.,-1.));
#5246=DIRECTION('ref_axis',(1.,0.,0.));
#5247=DIRECTION('center_axis',(0.,0.,-1.));
#5248=DIRECTION('ref_axis',(1.,0.,0.));
#5249=DIRECTION('',(0.707106781186548,8.65956056235494E-17,0.707106781186547));
#5250=DIRECTION('center_axis',(0.,0.,1.));
#5251=DIRECTION('ref_axis',(1.,0.,0.));
#5252=DIRECTION('center_axis',(0.,0.,1.));
#5253=DIRECTION('ref_axis',(1.,7.52212518638754E-14,0.));
#5254=DIRECTION('center_axis',(0.,0.,-1.));
#5255=DIRECTION('ref_axis',(1.,7.52212518638754E-14,0.));
#5256=DIRECTION('center_axis',(0.,0.,1.));
#5257=DIRECTION('ref_axis',(1.,0.,0.));
#5258=DIRECTION('center_axis',(-1.92296268638356E-16,-1.,0.));
#5259=DIRECTION('ref_axis',(1.,-1.92296268638356E-16,0.));
#5260=DIRECTION('',(1.,-1.92296268638356E-16,0.));
#5261=DIRECTION('',(0.,0.,1.));
#5262=DIRECTION('',(1.,-1.92296268638356E-16,0.));
#5263=DIRECTION('',(0.,0.,1.));
#5264=DIRECTION('center_axis',(-0.866025403784439,-0.5,0.));
#5265=DIRECTION('ref_axis',(0.5,-0.866025403784439,0.));
#5266=DIRECTION('',(0.5,-0.866025403784439,0.));
#5267=DIRECTION('',(0.,0.,1.));
#5268=DIRECTION('',(0.5,-0.866025403784439,0.));
#5269=DIRECTION('center_axis',(-0.866025403784439,0.5,0.));
#5270=DIRECTION('ref_axis',(-0.5,-0.866025403784438,0.));
#5271=DIRECTION('',(-0.5,-0.866025403784438,0.));
#5272=DIRECTION('',(0.,0.,1.));
#5273=DIRECTION('',(-0.5,-0.866025403784439,0.));
#5274=DIRECTION('center_axis',(1.92296268638356E-16,1.,0.));
#5275=DIRECTION('ref_axis',(-1.,1.92296268638356E-16,0.));
#5276=DIRECTION('',(-1.,1.92296268638356E-16,0.));
#5277=DIRECTION('',(0.,0.,1.));
#5278=DIRECTION('',(-1.,1.92296268638356E-16,0.));
#5279=DIRECTION('center_axis',(0.866025403784439,0.5,0.));
#5280=DIRECTION('ref_axis',(-0.5,0.866025403784439,0.));
#5281=DIRECTION('',(-0.5,0.866025403784439,0.));
#5282=DIRECTION('',(0.,0.,1.));
#5283=DIRECTION('',(-0.5,0.866025403784439,0.));
#5284=DIRECTION('center_axis',(0.866025403784439,-0.5,0.));
#5285=DIRECTION('ref_axis',(0.5,0.866025403784439,0.));
#5286=DIRECTION('',(0.5,0.866025403784439,0.));
#5287=DIRECTION('',(0.5,0.866025403784439,0.));
#5288=DIRECTION('center_axis',(0.,0.,1.));
#5289=DIRECTION('ref_axis',(1.,0.,0.));
#5290=DIRECTION('center_axis',(0.,0.,1.));
#5291=DIRECTION('ref_axis',(1.,0.,0.));
#5292=DIRECTION('center_axis',(0.,0.,1.));
#5293=DIRECTION('ref_axis',(1.,0.,0.));
#5294=DIRECTION('center_axis',(0.,0.,1.));
#5295=DIRECTION('ref_axis',(1.,0.,0.));
#5296=DIRECTION('',(0.,0.,-1.));
#5297=DIRECTION('center_axis',(0.,0.,1.));
#5298=DIRECTION('ref_axis',(1.,0.,0.));
#5299=DIRECTION('center_axis',(0.,0.,1.));
#5300=DIRECTION('ref_axis',(1.,0.,0.));
#5301=DIRECTION('center_axis',(0.,0.,1.));
#5302=DIRECTION('ref_axis',(1.,0.,0.));
#7681=CARTESIAN_POINT('',(0.,0.,0.));
#7682=CARTESIAN_POINT('Origin',(0.,0.,0.));
#7683=CARTESIAN_POINT('',(-2.94437861999191,0.00228824954296311,0.322176117089596));
#7684=CARTESIAN_POINT('',(-2.94436911647834,0.00312614869137163,0.177823882910396));
#7685=CARTESIAN_POINT('',(-2.942,-3.60291088309151E-16,0.));
#7686=CARTESIAN_POINT('',(1.28892185405323,2.64462557919717,0.));
#7687=CARTESIAN_POINT('Ctrl Pts',(-2.94437861999191,0.00228824954296311,
0.322176117089596));
#7688=CARTESIAN_POINT('Ctrl Pts',(-2.94551635113874,0.142778583613822,0.314557432409286));
#7689=CARTESIAN_POINT('Ctrl Pts',(-2.93631267309395,0.283111895578672,0.306938747728977));
#7690=CARTESIAN_POINT('Ctrl Pts',(-2.91624915612822,0.42186500989966,0.299320063048668));
#7691=CARTESIAN_POINT('Ctrl Pts',(-2.77830971889191,1.37581174500659,0.246940558544163));
#7692=CARTESIAN_POINT('Ctrl Pts',(-2.1270526803082,2.25506646395135,0.194561054039658));
#7693=CARTESIAN_POINT('Ctrl Pts',(-1.25475282359973,2.66583045735473,0.142181549535154));
#7694=CARTESIAN_POINT('Ctrl Pts',(-0.46548135530728,3.03749657388775,0.0947876996901026));
#7695=CARTESIAN_POINT('Ctrl Pts',(0.504756374147381,3.02561249996607,0.0473938498450515));
#7696=CARTESIAN_POINT('Ctrl Pts',(1.29197400994443,2.64783394680711,3.05745012640912E-16));
#7697=CARTESIAN_POINT('',(-1.28892185405326,2.64462557919716,0.));
#7698=CARTESIAN_POINT('Origin',(0.,0.,0.));
#7699=CARTESIAN_POINT('Ctrl Pts',(-1.28892185405326,2.64462557919716,1.87350135405495E-15));
#7700=CARTESIAN_POINT('Ctrl Pts',(-2.16038499609478,2.21989706654312,0.0524451052237091));
#7701=CARTESIAN_POINT('Ctrl Pts',(-2.79846764402885,1.33473338532309,0.104890210447416));
#7702=CARTESIAN_POINT('Ctrl Pts',(-2.92193100282573,0.379041548713593,0.157335315671123));
#7703=CARTESIAN_POINT('Ctrl Pts',(-2.93800868581449,0.25458915624929,0.164164838084214));
#7704=CARTESIAN_POINT('Ctrl Pts',(-2.94535953294187,0.128940758021734,0.170994360497305));
#7705=CARTESIAN_POINT('Ctrl Pts',(-2.94436911647834,0.00312614869137163,
0.177823882910396));
#7706=CARTESIAN_POINT('Origin',(0.,0.,0.));
#7707=CARTESIAN_POINT('',(-2.93740032720055,-0.000139020310086779,1.32217611708959));
#7708=CARTESIAN_POINT('',(-2.93737720095951,0.000230872487724698,1.1778238829104));
#7709=CARTESIAN_POINT('',(-2.942,-3.60291088309151E-16,0.));
#7710=CARTESIAN_POINT('Ctrl Pts',(-2.93740032720055,-0.000139020310086779,
1.32217611708959));
#7711=CARTESIAN_POINT('Ctrl Pts',(-2.93718361365059,0.494770241727901,1.29550112610298));
#7712=CARTESIAN_POINT('Ctrl Pts',(-2.81848923912434,0.989776479202536,1.26882613511636));
#7713=CARTESIAN_POINT('Ctrl Pts',(-2.58191143461274,1.4199490257311,1.24215114412975));
#7714=CARTESIAN_POINT('Ctrl Pts',(-2.11736289237333,2.26464377557798,1.18977163962524));
#7715=CARTESIAN_POINT('Ctrl Pts',(-1.19827972440715,2.85935294685526,1.13739213512074));
#7716=CARTESIAN_POINT('Ctrl Pts',(-0.2374000875181,2.93702585155106,1.08501263061624));
#7717=CARTESIAN_POINT('Ctrl Pts',(0.723479549370952,3.01469875624685,1.03263312611173));
#7718=CARTESIAN_POINT('Ctrl Pts',(1.72615565518287,2.57533539436116,0.980253621607226));
#7719=CARTESIAN_POINT('Ctrl Pts',(2.32033868002489,1.8162041612206,0.927874117102722));
#7720=CARTESIAN_POINT('Ctrl Pts',(2.9145217048669,1.05707292808004,0.875494612598217));
#7721=CARTESIAN_POINT('Ctrl Pts',(3.100211648739,-0.0218261763153739,0.823115108093712));
#7722=CARTESIAN_POINT('Ctrl Pts',(2.79403320730894,-0.935902477435646,0.770735603589208));
#7723=CARTESIAN_POINT('Ctrl Pts',(2.48785476587888,-1.84997877855592,0.718356099084703));
#7724=CARTESIAN_POINT('Ctrl Pts',(1.68980793914667,-2.59923227640105,0.665976594580199));
#7725=CARTESIAN_POINT('Ctrl Pts',(0.75825229618776,-2.84733793424016,0.613597090075694));
#7726=CARTESIAN_POINT('Ctrl Pts',(-0.173303346771145,-3.09544359207927,
0.56121758557119));
#7727=CARTESIAN_POINT('Ctrl Pts',(-1.23836780595674,-2.84240140991237,0.508838081066685));
#7728=CARTESIAN_POINT('Ctrl Pts',(-1.95858911760509,-2.20156094319437,0.456458576562181));
#7729=CARTESIAN_POINT('Ctrl Pts',(-2.57405306040479,-1.65393177147606,0.411697756737986));
#7730=CARTESIAN_POINT('Ctrl Pts',(-2.93769429310237,-0.823111776086056,
0.366936936913791));
#7731=CARTESIAN_POINT('Ctrl Pts',(-2.94437861999191,0.00228824954296311,
0.322176117089596));
#7732=CARTESIAN_POINT('Ctrl Pts',(-2.94436911647834,0.00312614869137163,
0.177823882910396));
#7733=CARTESIAN_POINT('Ctrl Pts',(-2.93775395051561,-0.837211781775621,
0.223439465721013));
#7734=CARTESIAN_POINT('Ctrl Pts',(-2.55902339432207,-1.68496462111194,0.26905504853163));
#7735=CARTESIAN_POINT('Ctrl Pts',(-1.92306539600717,-2.23328718212897,0.314670631342247));
#7736=CARTESIAN_POINT('Ctrl Pts',(-1.19189236073203,-2.86370408436305,0.367115736565955));
#7737=CARTESIAN_POINT('Ctrl Pts',(-0.120702220522052,-3.09831789683223,
0.419560841789662));
#7738=CARTESIAN_POINT('Ctrl Pts',(0.807638005699694,-2.8335361097114,0.47200594701337));
#7739=CARTESIAN_POINT('Ctrl Pts',(1.73597823192144,-2.56875432259058,0.524451052237078));
#7740=CARTESIAN_POINT('Ctrl Pts',(2.52146854415495,-1.80457693587975,0.576896157460787));
#7741=CARTESIAN_POINT('Ctrl Pts',(2.81091642121069,-0.883954119006901,0.629341262684494));
#7742=CARTESIAN_POINT('Ctrl Pts',(3.10036429826643,0.0366686978659464,0.681786367908202));
#7743=CARTESIAN_POINT('Ctrl Pts',(2.89376974014439,1.11373694490081,0.734231473131909));
#7744=CARTESIAN_POINT('Ctrl Pts',(2.28393241469019,1.86192138048068,0.786676578355617));
#7745=CARTESIAN_POINT('Ctrl Pts',(1.674095089236,2.61010581606054,0.839121683579324));
#7746=CARTESIAN_POINT('Ctrl Pts',(0.661014996449636,3.02940644018541,0.891566788803033));
#7747=CARTESIAN_POINT('Ctrl Pts',(-0.299207810136722,2.93136603044105,0.944011894026741));
#7748=CARTESIAN_POINT('Ctrl Pts',(-1.25943061672308,2.83332562069669,0.996456999250449));
#7749=CARTESIAN_POINT('Ctrl Pts',(-2.16679613710945,2.21794417708309,1.04890210447416));
#7750=CARTESIAN_POINT('Ctrl Pts',(-2.61293993368518,1.36206873790977,1.10134720969786));
#7751=CARTESIAN_POINT('Ctrl Pts',(-2.82979902340055,0.946049575313678,1.12683943410204));
#7752=CARTESIAN_POINT('Ctrl Pts',(-2.93768601866802,0.47320929383844,1.15233165850622));
#7753=CARTESIAN_POINT('Ctrl Pts',(-2.93737720095951,0.000230872487724698,
1.1778238829104));
#7754=CARTESIAN_POINT('Origin',(0.,0.,0.));
#7755=CARTESIAN_POINT('',(-2.94487182720719,-0.00190539986535287,2.32217611708959));
#7756=CARTESIAN_POINT('',(-2.94409804542743,-0.00221960462873976,2.1778238829104));
#7757=CARTESIAN_POINT('',(-2.942,-3.60291088309151E-16,0.));
#7758=CARTESIAN_POINT('Ctrl Pts',(-2.94487182720719,-0.00190539986535287,
2.32217611708959));
#7759=CARTESIAN_POINT('Ctrl Pts',(-2.93849254859689,0.841069663508672,2.27644481979667));
#7760=CARTESIAN_POINT('Ctrl Pts',(-2.55692453936773,1.68909389771769,2.23071352250375));
#7761=CARTESIAN_POINT('Ctrl Pts',(-1.91797659724234,2.23693579382214,2.18498222521083));
#7762=CARTESIAN_POINT('Ctrl Pts',(-1.18614132044426,2.86442044357863,2.13260272070633));
#7763=CARTESIAN_POINT('Ctrl Pts',(-0.116653199765081,3.09810042098425,2.08022321620182));
#7764=CARTESIAN_POINT('Ctrl Pts',(0.810201861614963,2.83303510458914,2.02784371169732));
#7765=CARTESIAN_POINT('Ctrl Pts',(1.73705692299501,2.56796978819403,1.97546420719281));
#7766=CARTESIAN_POINT('Ctrl Pts',(2.52127892507592,1.80415917799819,1.92308470268831));
#7767=CARTESIAN_POINT('Ctrl Pts',(2.81068910755427,0.88461468761641,1.8707051981838));
#7768=CARTESIAN_POINT('Ctrl Pts',(3.10009929003262,-0.0349298027653776,
1.8183256936793));
#7769=CARTESIAN_POINT('Ctrl Pts',(2.89469765290841,-1.11020817333311,1.76594618917479));
#7770=CARTESIAN_POINT('Ctrl Pts',(2.28672630753671,-1.85833254788295,1.71356668467029));
#7771=CARTESIAN_POINT('Ctrl Pts',(1.67875496216501,-2.60645692243279,1.66118718016578));
#7772=CARTESIAN_POINT('Ctrl Pts',(0.668213908545816,-3.02742730096473,1.60880767566128));
#7773=CARTESIAN_POINT('Ctrl Pts',(-0.291083395731117,-2.93219727380604,
1.55642817115678));
#7774=CARTESIAN_POINT('Ctrl Pts',(-1.25038070000804,-2.83696724664735,1.50404866665227));
#7775=CARTESIAN_POINT('Ctrl Pts',(-2.15843425494271,-2.22553681379804,1.45166916214777));
#7776=CARTESIAN_POINT('Ctrl Pts',(-2.60745407415374,-1.37248143316515,1.39928965764326));
#7777=CARTESIAN_POINT('Ctrl Pts',(-2.82780430697652,-0.953856366540085,
1.37358514412537));
#7778=CARTESIAN_POINT('Ctrl Pts',(-2.93760915637607,-0.477042717206063,
1.34788063060748));
#7779=CARTESIAN_POINT('Ctrl Pts',(-2.93740032720055,-0.000139020310086779,
1.32217611708959));
#7780=CARTESIAN_POINT('Ctrl Pts',(-2.93737720095951,0.000230872487724698,
1.1778238829104));
#7781=CARTESIAN_POINT('Ctrl Pts',(-2.9370506885783,-0.499848321024544,1.20477676372993));
#7782=CARTESIAN_POINT('Ctrl Pts',(-2.81577431600542,-1.00008193824477,1.23172964454946));
#7783=CARTESIAN_POINT('Ctrl Pts',(-2.57446559490686,-1.43347457044749,1.25868252536899));
#7784=CARTESIAN_POINT('Ctrl Pts',(-2.10492538678771,-2.27677300489839,1.31112763059269));
#7785=CARTESIAN_POINT('Ctrl Pts',(-1.1809228977843,-2.86700043906715,1.3635727358164));
#7786=CARTESIAN_POINT('Ctrl Pts',(-0.218377608724914,-2.93852741234213,
1.41601784104011));
#7787=CARTESIAN_POINT('Ctrl Pts',(0.744167680334467,-3.01005438561711,1.46846294626382));
#7788=CARTESIAN_POINT('Ctrl Pts',(1.74525576944982,-2.56288089799832,1.52090805148753));
#7789=CARTESIAN_POINT('Ctrl Pts',(2.33429173832943,-1.79826479808332,1.57335315671123));
#7790=CARTESIAN_POINT('Ctrl Pts',(2.92332770720905,-1.03364869816832,1.62579826193494));
#7791=CARTESIAN_POINT('Ctrl Pts',(3.10031155585293,0.0484100140428809,1.67824336715865));
#7792=CARTESIAN_POINT('Ctrl Pts',(2.78557670999694,0.960852278151669,1.73068847238236));
#7793=CARTESIAN_POINT('Ctrl Pts',(2.47084186414094,1.87329454226046,1.78313357760607));
#7794=CARTESIAN_POINT('Ctrl Pts',(1.66438832378506,2.61612035826684,1.83557868282977));
#7795=CARTESIAN_POINT('Ctrl Pts',(0.729213057861966,2.85498007465664,1.88802378805348));
#7796=CARTESIAN_POINT('Ctrl Pts',(-0.205962208061124,3.09383979104644,1.94046889327719));
#7797=CARTESIAN_POINT('Ctrl Pts',(-1.26985919955142,2.82873340781965,1.9929139985009));
#7798=CARTESIAN_POINT('Ctrl Pts',(-1.98360551176881,2.17898571169394,2.0453591037246));
#7799=CARTESIAN_POINT('Ctrl Pts',(-2.58452748049057,1.63194587688865,2.08951403011987));
#7800=CARTESIAN_POINT('Ctrl Pts',(-2.93724853244873,0.81225677381718,2.13366895651513));
#7801=CARTESIAN_POINT('Ctrl Pts',(-2.94409804542743,-0.00221960462873976,
2.1778238829104));
#7802=CARTESIAN_POINT('Origin',(0.,0.,0.));
#7803=CARTESIAN_POINT('',(-2.94188729812012,0.00254759896953657,3.32217611708959));
#7804=CARTESIAN_POINT('',(-2.94300132914192,0.00247067809074119,3.17782388291039));
#7805=CARTESIAN_POINT('',(-2.942,-3.60291088309151E-16,0.));
#7806=CARTESIAN_POINT('Ctrl Pts',(-2.94188729812012,0.00254759896953657,
3.32217611708959));
#7807=CARTESIAN_POINT('Ctrl Pts',(-2.94391723822425,0.231870355671395,3.30976801799487));
#7808=CARTESIAN_POINT('Ctrl Pts',(-2.91930872547992,0.460762551320829,3.29735991890015));
#7809=CARTESIAN_POINT('Ctrl Pts',(-2.86638309031571,0.682908266801983,3.28495181980542));
#7810=CARTESIAN_POINT('Ctrl Pts',(-2.64296300603654,1.62067338423639,3.23257231530092));
#7811=CARTESIAN_POINT('Ctrl Pts',(-1.91492649555138,2.438214961245,3.18019281079642));
#7812=CARTESIAN_POINT('Ctrl Pts',(-1.00922037183541,2.76839122410029,3.12781330629191));
#7813=CARTESIAN_POINT('Ctrl Pts',(-0.103514248119433,3.09856748695557,3.07543380178741));
#7814=CARTESIAN_POINT('Ctrl Pts',(0.979861488827348,2.94137843565753,3.0230542972829));
#7815=CARTESIAN_POINT('Ctrl Pts',(1.75438420282982,2.3674145763557,2.9706747927784));
#7816=CARTESIAN_POINT('Ctrl Pts',(2.5289069168323,1.79345071705387,2.91829528827389));
#7817=CARTESIAN_POINT('Ctrl Pts',(2.99457660789046,0.802712049748258,2.86591578376939));
#7818=CARTESIAN_POINT('Ctrl Pts',(2.94227021542597,-0.159880282562335,2.81353627926488));
#7819=CARTESIAN_POINT('Ctrl Pts',(2.88996382296149,-1.12247261487293,2.76115677476038));
#7820=CARTESIAN_POINT('Ctrl Pts',(2.31968134697434,-2.0569186121885,2.70877727025587));
#7821=CARTESIAN_POINT('Ctrl Pts',(1.48752538566269,-2.54357700727495,2.65639776575137));
#7822=CARTESIAN_POINT('Ctrl Pts',(0.655369424351043,-3.0302354023614,2.60401826124687));
#7823=CARTESIAN_POINT('Ctrl Pts',(-0.438660022285117,-3.06910619521874,
2.55163875674236));
#7824=CARTESIAN_POINT('Ctrl Pts',(-1.30325595742871,-2.64273334365957,2.49925925223786));
#7825=CARTESIAN_POINT('Ctrl Pts',(-2.1678518925723,-2.21636049210041,2.44687974773335));
#7826=CARTESIAN_POINT('Ctrl Pts',(-2.80301431622333,-1.32474399612474,2.39450024322885));
#7827=CARTESIAN_POINT('Ctrl Pts',(-2.92350431159035,-0.368291087083228,
2.34212073872434));
#7828=CARTESIAN_POINT('Ctrl Pts',(-2.93879736301763,-0.246894422727957,
2.33547253151276));
#7829=CARTESIAN_POINT('Ctrl Pts',(-2.94579921760659,-0.124453265927633,
2.32882432430118));
#7830=CARTESIAN_POINT('Ctrl Pts',(-2.94487182720719,-0.00190539986535287,
2.32217611708959));
#7831=CARTESIAN_POINT('Ctrl Pts',(-2.94409804542743,-0.00221960462873976,
2.1778238829104));
#7832=CARTESIAN_POINT('Ctrl Pts',(-2.94538405566721,-0.155139230593375,
2.18611406173884));
#7833=CARTESIAN_POINT('Ctrl Pts',(-2.93447780370748,-0.307875103637501,
2.19440424056728));
#7834=CARTESIAN_POINT('Ctrl Pts',(-2.91073286453113,-0.458588216909009,
2.20269441939573));
#7835=CARTESIAN_POINT('Ctrl Pts',(-2.76051827213159,-1.41202544036162,2.25513952461944));
#7836=CARTESIAN_POINT('Ctrl Pts',(-2.09649345438802,-2.28451087824219,2.30758462984315));
#7837=CARTESIAN_POINT('Ctrl Pts',(-1.21754466145652,-2.68332862013697,2.36002973506685));
#7838=CARTESIAN_POINT('Ctrl Pts',(-0.338595868525027,-3.08214636203174,
2.41247484029056));
#7839=CARTESIAN_POINT('Ctrl Pts',(0.755276899594388,-3.00729640794073,2.46491994551426));
#7840=CARTESIAN_POINT('Ctrl Pts',(1.57170784623814,-2.49246924635079,2.51736505073797));
#7841=CARTESIAN_POINT('Ctrl Pts',(2.3881387928819,-1.97764208476085,2.56981015596168));
#7842=CARTESIAN_POINT('Ctrl Pts',(2.92712791805,-1.02283771567197,2.62225526118539));
#7843=CARTESIAN_POINT('Ctrl Pts',(2.94606932856971,-0.0578258660348382,
2.6747003664091));
#7844=CARTESIAN_POINT('Ctrl Pts',(2.96501073908941,0.907185983602299,2.72714547163281));
#7845=CARTESIAN_POINT('Ctrl Pts',(2.46390443496074,1.88240531378769,2.77959057685651));
#7846=CARTESIAN_POINT('Ctrl Pts',(1.66830473495772,2.42887370127543,2.83203568208022));
#7847=CARTESIAN_POINT('Ctrl Pts',(0.872705034954712,2.97534208876317,2.88448078730393));
#7848=CARTESIAN_POINT('Ctrl Pts',(-0.217388060922636,3.09305953355326,2.93692589252764));
#7849=CARTESIAN_POINT('Ctrl Pts',(-1.11130990317228,2.72903986659667,2.98937099775135));
#7850=CARTESIAN_POINT('Ctrl Pts',(-2.00523174542191,2.36502019964009,3.04181610297505));
#7851=CARTESIAN_POINT('Ctrl Pts',(-2.70298233404385,1.51926342093683,3.09426120819876));
#7852=CARTESIAN_POINT('Ctrl Pts',(-2.89049530439613,0.572455370821353,3.14670631342247));
#7853=CARTESIAN_POINT('Ctrl Pts',(-2.92758137029262,0.385196933861252,3.15707883658511));
#7854=CARTESIAN_POINT('Ctrl Pts',(-2.94470877622731,0.1939857347123,3.16745135974775));
#7855=CARTESIAN_POINT('Ctrl Pts',(-2.94300132914192,0.00247067809074119,
3.17782388291039));
#7856=CARTESIAN_POINT('Origin',(0.,0.,0.));
#7857=CARTESIAN_POINT('',(-2.93815144027097,-0.00144838940242836,4.32217611708959));
#7858=CARTESIAN_POINT('',(-2.93758805006728,-0.000810565913221897,4.1778238829104));
#7859=CARTESIAN_POINT('',(-2.942,-3.60291088309151E-16,0.));
#7860=CARTESIAN_POINT('Ctrl Pts',(-2.93815144027097,-0.00144838940242836,
4.32217611708959));
#7861=CARTESIAN_POINT('Ctrl Pts',(-2.93549507201127,0.581944663119171,4.29071171168856));
#7862=CARTESIAN_POINT('Ctrl Pts',(-2.76704590305946,1.16675179323199,4.25924730628754));
#7863=CARTESIAN_POINT('Ctrl Pts',(-2.44338137442995,1.64693751569171,4.22778290088651));
#7864=CARTESIAN_POINT('Ctrl Pts',(-1.90456974207211,2.44631350554451,4.175403396382));
#7865=CARTESIAN_POINT('Ctrl Pts',(-0.93560961338887,2.95575207374732,4.1230238918775));
#7866=CARTESIAN_POINT('Ctrl Pts',(0.0283581627927666,2.94647442485208,4.07064438737299));
#7867=CARTESIAN_POINT('Ctrl Pts',(0.992325938974403,2.93719677595684,4.01826488286848));
#7868=CARTESIAN_POINT('Ctrl Pts',(1.95130136265442,2.40920290996356,3.96588537836398));
#7869=CARTESIAN_POINT('Ctrl Pts',(2.4746275187937,1.59960444002515,3.91350587385948));
#7870=CARTESIAN_POINT('Ctrl Pts',(2.99795367493297,0.790005970086747,3.86112636935497));
#7871=CARTESIAN_POINT('Ctrl Pts',(3.0856305635315,-0.301197103796779,3.80874686485047));
#7872=CARTESIAN_POINT('Ctrl Pts',(2.69828422619929,-1.18396704178881,3.75636736034596));
#7873=CARTESIAN_POINT('Ctrl Pts',(2.31093788886708,-2.06673697978085,3.70398785584146));
#7874=CARTESIAN_POINT('Ctrl Pts',(1.44856832560414,-2.7410737818814,3.65160835133695));
#7875=CARTESIAN_POINT('Ctrl Pts',(0.498448668458934,-2.90414611332682,3.59922884683245));
#7876=CARTESIAN_POINT('Ctrl Pts',(-0.451670988686273,-3.06721844477224,
3.54684934232795));
#7877=CARTESIAN_POINT('Ctrl Pts',(-1.48954073971375,-2.71902630556253,3.49446983782344));
#7878=CARTESIAN_POINT('Ctrl Pts',(-2.1490737861909,-2.01593590702758,3.44209033331894));
#7879=CARTESIAN_POINT('Ctrl Pts',(-2.65237107835254,-1.47939949597489,3.40211892790916));
#7880=CARTESIAN_POINT('Ctrl Pts',(-2.93534805643284,-0.736191897535303,
3.36214752249938));
#7881=CARTESIAN_POINT('Ctrl Pts',(-2.94188729812012,0.00254759896953657,
3.32217611708959));
#7882=CARTESIAN_POINT('Ctrl Pts',(-2.94300132914192,0.00247067809074119,
3.17782388291039));
#7883=CARTESIAN_POINT('Ctrl Pts',(-2.93607565575577,-0.774344452547842,
3.21989646497146));
#7884=CARTESIAN_POINT('Ctrl Pts',(-2.61927127105561,-1.55615877069983,3.26196904703253));
#7885=CARTESIAN_POINT('Ctrl Pts',(-2.06758380697847,-2.0994678941542,3.30404162909359));
#7886=CARTESIAN_POINT('Ctrl Pts',(-1.37988398712591,-2.77672378748653,3.3564867343173));
#7887=CARTESIAN_POINT('Ctrl Pts',(-0.327208995338195,-3.08337625262348,
3.40893183954101));
#7888=CARTESIAN_POINT('Ctrl Pts',(0.616618861412321,-2.88139713307019,3.46137694476472));
#7889=CARTESIAN_POINT('Ctrl Pts',(1.56044671816283,-2.67941801351691,3.51382204998842));
#7890=CARTESIAN_POINT('Ctrl Pts',(2.39542743987614,-1.9688073092734,3.56626715521213));
#7891=CARTESIAN_POINT('Ctrl Pts',(2.74572565546219,-1.06941987852551,3.61871226043584));
#7892=CARTESIAN_POINT('Ctrl Pts',(3.09602387104824,-0.170032447777603,3.67115736565955));
#7893=CARTESIAN_POINT('Ctrl Pts',(2.96163958050702,0.918131709474696,3.72360247088326));
#7894=CARTESIAN_POINT('Ctrl Pts',(2.40306085127007,1.70527616384954,3.77604757610696));
#7895=CARTESIAN_POINT('Ctrl Pts',(1.84448212203313,2.49242061822439,3.82849268133067));
#7896=CARTESIAN_POINT('Ctrl Pts',(0.86170895410048,2.97854536972178,3.88093778655438));
#7897=CARTESIAN_POINT('Ctrl Pts',(-0.10290003671811,2.94483952623603,3.93338289177809));
#7898=CARTESIAN_POINT('Ctrl Pts',(-1.06750902753671,2.91113368275028,3.98582799700179));
#7899=CARTESIAN_POINT('Ctrl Pts',(-2.01395384124124,2.35759724428137,4.0382731022255));
#7900=CARTESIAN_POINT('Ctrl Pts',(-2.51622771244025,1.53338395412712,4.09071820744921));
#7901=CARTESIAN_POINT('Ctrl Pts',(-2.79430199366995,1.07707409733029,4.11975343260294));
#7902=CARTESIAN_POINT('Ctrl Pts',(-2.9362347477918,0.537799876108109,4.14878865775667));
#7903=CARTESIAN_POINT('Ctrl Pts',(-2.93758805006728,-0.000810565913221897,
4.1778238829104));
#7904=CARTESIAN_POINT('Origin',(0.,0.,0.));
#7905=CARTESIAN_POINT('',(-2.94644869531747,-0.000604754645607275,5.3221761170896));
#7906=CARTESIAN_POINT('',(-2.945679792052,-0.00146169071580815,5.1778238829104));
#7907=CARTESIAN_POINT('',(-2.942,-3.60291088309151E-16,0.));
#7908=CARTESIAN_POINT('Ctrl Pts',(-2.94644869531747,-0.000604754645607275,
5.3221761170896));
#7909=CARTESIAN_POINT('Ctrl Pts',(-2.94379550054715,0.929335583914262,5.27165540538226));
#7910=CARTESIAN_POINT('Ctrl Pts',(-2.46604729438678,1.86162808593007,5.22113469367492));
#7911=CARTESIAN_POINT('Ctrl Pts',(-1.70849336410036,2.40074283220066,5.17061398196758));
#7912=CARTESIAN_POINT('Ctrl Pts',(-0.923066988207087,2.95969305927406,5.11823447746308));
#7913=CARTESIAN_POINT('Ctrl Pts',(0.163133494924937,3.09600115191732,5.06585497295858));
#7914=CARTESIAN_POINT('Ctrl Pts',(1.06231690977038,2.74845383893534,5.01347546845407));
#7915=CARTESIAN_POINT('Ctrl Pts',(1.96150032461582,2.40090652595338,4.96109596394957));
#7916=CARTESIAN_POINT('Ctrl Pts',(2.67366667117468,1.56950380734618,4.90871645944506));
#7917=CARTESIAN_POINT('Ctrl Pts',(2.87899611438783,0.627612216959094,4.85633695494056));
#7918=CARTESIAN_POINT('Ctrl Pts',(3.08432555760098,-0.314279373428012,4.80395745043605));
#7919=CARTESIAN_POINT('Ctrl Pts',(2.7828180974684,-1.36665983559502,4.75157794593155));
#7920=CARTESIAN_POINT('Ctrl Pts',(2.10987477706647,-2.05692589721429,4.69919844142705));
#7921=CARTESIAN_POINT('Ctrl Pts',(1.43693145666455,-2.74719195883355,4.64681893692254));
#7922=CARTESIAN_POINT('Ctrl Pts',(0.392552275993288,-3.07534361990509,4.59443943241804));
#7923=CARTESIAN_POINT('Ctrl Pts',(-0.554252710038128,-2.89401445313919,
4.54205992791353));
#7924=CARTESIAN_POINT('Ctrl Pts',(-1.50105769606954,-2.71268528637328,4.48968042340903));
#7925=CARTESIAN_POINT('Ctrl Pts',(-2.35028848746111,-2.02187529176995,4.43730091890452));
#7926=CARTESIAN_POINT('Ctrl Pts',(-2.72057231514067,-1.13181358871689,4.38492141440002));
#7927=CARTESIAN_POINT('Ctrl Pts',(-2.86842638565151,-0.776412580180032,
4.36400631529654));
#7928=CARTESIAN_POINT('Ctrl Pts',(-2.93991718809614,-0.389242894153138,
4.34309121619307));
#7929=CARTESIAN_POINT('Ctrl Pts',(-2.93815144027097,-0.00144838940242836,
4.32217611708959));
#7930=CARTESIAN_POINT('Ctrl Pts',(-2.93758805006728,-0.000810565913221897,
4.1778238829104));
#7931=CARTESIAN_POINT('Ctrl Pts',(-2.93867916073716,-0.435069497448956,
4.20123376298038));
#7932=CARTESIAN_POINT('Ctrl Pts',(-2.84838634229403,-0.86889693810433,4.22464364305035));
#7933=CARTESIAN_POINT('Ctrl Pts',(-2.66438363654231,-1.25846258937073,4.24805352312033));
#7934=CARTESIAN_POINT('Ctrl Pts',(-2.25216276075188,-2.13120570087471,4.30049862834404));
#7935=CARTESIAN_POINT('Ctrl Pts',(-1.36961808047753,-2.78180178204309,4.35294373356775));
#7936=CARTESIAN_POINT('Ctrl Pts',(-0.413994103635433,-2.91740931891088,
4.40538883879146));
#7937=CARTESIAN_POINT('Ctrl Pts',(0.541629873206673,-3.05301685577867,4.45783394401517));
#7938=CARTESIAN_POINT('Ctrl Pts',(1.57033314661653,-2.67363584834587,4.51027904923887));
#7939=CARTESIAN_POINT('Ctrl Pts',(2.20908337968645,-1.9500304800975,4.56272415446258));
#7940=CARTESIAN_POINT('Ctrl Pts',(2.84783361275636,-1.22642511184914,4.61516925968629));
#7941=CARTESIAN_POINT('Ctrl Pts',(3.09663080548633,-0.158595382785209,4.66761436491));
#7942=CARTESIAN_POINT('Ctrl Pts',(2.84348819889812,0.772815058373636,4.7200594701337));
#7943=CARTESIAN_POINT('Ctrl Pts',(2.5903455923099,1.70422549953248,4.77250457535741));
#7944=CARTESIAN_POINT('Ctrl Pts',(1.83526318640351,2.49921665278624,4.82494968058112));
#7945=CARTESIAN_POINT('Ctrl Pts',(0.918113109485756,2.79995295852677,4.87739478580482));
#7946=CARTESIAN_POINT('Ctrl Pts',(0.000963032567994487,3.1006892642673,
4.92983989102853));
#7947=CARTESIAN_POINT('Ctrl Pts',(-1.07825471536113,2.90717072249458,4.98228499625224));
#7948=CARTESIAN_POINT('Ctrl Pts',(-1.83377059439506,2.30650247319915,5.03473010147595));
#7949=CARTESIAN_POINT('Ctrl Pts',(-2.5208993779335,1.76020496324304,5.08242802862077));
#7950=CARTESIAN_POINT('Ctrl Pts',(-2.94027519175655,0.877129838501974,5.13012595576559));
#7951=CARTESIAN_POINT('Ctrl Pts',(-2.945679792052,-0.00146169071580815,
5.1778238829104));
#7952=CARTESIAN_POINT('Origin',(0.,0.,0.));
#7953=CARTESIAN_POINT('',(-2.93949980478958,0.00219056232359141,6.3221761170896));
#7954=CARTESIAN_POINT('',(-2.94109090649655,0.00253660757586993,6.1778238829104));
#7955=CARTESIAN_POINT('',(-2.942,-3.60291088309151E-16,0.));
#7956=CARTESIAN_POINT('Ctrl Pts',(-2.93949980478958,0.00219056232359141,
6.3221761170896));
#7957=CARTESIAN_POINT('Ctrl Pts',(-2.94176361798241,0.320687415620876,6.30497860358046));
#7958=CARTESIAN_POINT('Ctrl Pts',(-2.89395610782771,0.638523376129415,6.28778109007132));
#7959=CARTESIAN_POINT('Ctrl Pts',(-2.79314214575126,0.938548174128603,6.27058357656218));
#7960=CARTESIAN_POINT('Ctrl Pts',(-2.48608697885785,1.85235180335153,6.21820407205768));
#7961=CARTESIAN_POINT('Ctrl Pts',(-1.68730919078036,2.60092740470414,6.16582456755317));
#7962=CARTESIAN_POINT('Ctrl Pts',(-0.75552410366601,2.84810446618733,6.11344506304867));
#7963=CARTESIAN_POINT('Ctrl Pts',(0.176260983448343,3.09528152767051,6.06106555854416));
#7964=CARTESIAN_POINT('Ctrl Pts',(1.24105336959955,2.84106004928427,6.00868605403966));
#7965=CARTESIAN_POINT('Ctrl Pts',(1.96067583262663,2.19960587399116,5.95630654953515));
#7966=CARTESIAN_POINT('Ctrl Pts',(2.68029829565369,1.55815169869806,5.90392704503064));
#7967=CARTESIAN_POINT('Ctrl Pts',(3.05475083555665,0.52946482649812,5.85154754052614));
#7968=CARTESIAN_POINT('Ctrl Pts',(2.91587421520356,-0.424491793382225,5.79916803602164));
#7969=CARTESIAN_POINT('Ctrl Pts',(2.77699759485047,-1.37844841326258,5.74678853151713));
#7970=CARTESIAN_POINT('Ctrl Pts',(2.12479181424134,-2.25767478082334,5.69440902701263));
#7971=CARTESIAN_POINT('Ctrl Pts',(1.25214960298458,-2.66732770639159,5.64202952250812));
#7972=CARTESIAN_POINT('Ctrl Pts',(0.379507391727844,-3.07698063195983,5.58965001800362));
#7973=CARTESIAN_POINT('Ctrl Pts',(-0.713571250176501,-3.01706011553558,
5.53727051349912));
#7974=CARTESIAN_POINT('Ctrl Pts',(-1.53620630199898,-2.5144752771182,5.48489100899462));
#7975=CARTESIAN_POINT('Ctrl Pts',(-2.35884135382146,-2.01189043870081,5.43251150449011));
#7976=CARTESIAN_POINT('Ctrl Pts',(-2.91103281556208,-1.0666412782903,5.3801319999856));
#7977=CARTESIAN_POINT('Ctrl Pts',(-2.94480241210512,-0.103220517333276,
5.3277524954811));
#7978=CARTESIAN_POINT('Ctrl Pts',(-2.94600079462919,-0.069031580495304,
5.32589370268393));
#7979=CARTESIAN_POINT('Ctrl Pts',(-2.94654631348559,-0.0348197596345374,
5.32403490988676));
#7980=CARTESIAN_POINT('Ctrl Pts',(-2.94644869531747,-0.000604754645607275,
5.3221761170896));
#7981=CARTESIAN_POINT('Ctrl Pts',(-2.945679792052,-0.00146169071580815,
5.1778238829104));
#7982=CARTESIAN_POINT('Ctrl Pts',(-2.94621768964176,-0.0889042840834332,
5.18257106098929));
#7983=CARTESIAN_POINT('Ctrl Pts',(-2.94265503660913,-0.176302465642187,
5.18731823906819));
#7984=CARTESIAN_POINT('Ctrl Pts',(-2.93484768462379,-0.263319805187537,
5.19206541714708));
#7985=CARTESIAN_POINT('Ctrl Pts',(-2.84859488567985,-1.22465587746066,5.24451052237078));
#7986=CARTESIAN_POINT('Ctrl Pts',(-2.24427527765324,-2.13951006518879,5.29695562759449));
#7987=CARTESIAN_POINT('Ctrl Pts',(-1.39390074925371,-2.59609494298297,5.34940073281819));
#7988=CARTESIAN_POINT('Ctrl Pts',(-0.543526220854162,-3.05267982077716,
5.4018458380419));
#7989=CARTESIAN_POINT('Ctrl Pts',(0.552903227918311,-3.05099538863739,5.45429094326562));
#7990=CARTESIAN_POINT('Ctrl Pts',(1.40187085321134,-2.59179983074767,5.50673604848932));
#7991=CARTESIAN_POINT('Ctrl Pts',(2.25083847850436,-2.13260427285796,5.55918115371303));
#7992=CARTESIAN_POINT('Ctrl Pts',(2.85234428031795,-1.21589758921833,5.61162625893673));
#7993=CARTESIAN_POINT('Ctrl Pts',(2.93564289965894,-0.254301037021637,5.66407136416044));
#7994=CARTESIAN_POINT('Ctrl Pts',(3.01894151899992,0.707295515175046,5.71651646938415));
#7995=CARTESIAN_POINT('Ctrl Pts',(2.5840329558683,1.71378193592877,5.76896157460786));
#7996=CARTESIAN_POINT('Ctrl Pts',(1.82667504784324,2.31212597436553,5.82140667983157));
#7997=CARTESIAN_POINT('Ctrl Pts',(1.06931713981816,2.9104700128023,5.87385178505528));
#7998=CARTESIAN_POINT('Ctrl Pts',(-0.010490113100349,3.1006716689221,5.92629689027898));
#7999=CARTESIAN_POINT('Ctrl Pts',(-0.92671182736886,2.79711877487579,5.97874199550269));
#8000=CARTESIAN_POINT('Ctrl Pts',(-1.84293354163737,2.49356588082949,6.0311871007264));
#8001=CARTESIAN_POINT('Ctrl Pts',(-2.59556971725588,1.69625843661705,6.08363220595011));
#8002=CARTESIAN_POINT('Ctrl Pts',(-2.84584930505901,0.764074593638618,6.13607731117382));
#8003=CARTESIAN_POINT('Ctrl Pts',(-2.91225724864025,0.516733559576513,6.14999283508601));
#8004=CARTESIAN_POINT('Ctrl Pts',(-2.94329794130529,0.259896865352817,6.16390835899821));
#8005=CARTESIAN_POINT('Ctrl Pts',(-2.94109090649655,0.00253660757586993,
6.1778238829104));
#8006=CARTESIAN_POINT('Origin',(0.,0.,0.));
#8007=CARTESIAN_POINT('',(-2.93998607517527,-0.0023358300504342,7.3221761170896));
#8008=CARTESIAN_POINT('',(-2.93846014819028,-0.00170708260597003,7.1778238829104));
#8009=CARTESIAN_POINT('',(-2.942,-3.60291088309151E-16,0.));
#8010=CARTESIAN_POINT('Ctrl Pts',(-2.93998607517527,-0.0023358300504342,
7.3221761170896));
#8011=CARTESIAN_POINT('Ctrl Pts',(-2.93483565594967,0.668801419715884,7.28592229727415));
#8012=CARTESIAN_POINT('Ctrl Pts',(-2.70624449366069,1.34311250814063,7.2496684774587));
#8013=CARTESIAN_POINT('Ctrl Pts',(-2.28495024526271,1.86051554631288,7.21341465764326));
#8014=CARTESIAN_POINT('Ctrl Pts',(-1.67626448210673,2.60805925085354,7.16103515313876));
#8015=CARTESIAN_POINT('Ctrl Pts',(-0.665321452888303,3.02806588999372,7.10865564863425));
#8016=CARTESIAN_POINT('Ctrl Pts',(0.293884302746592,2.93191878092119,7.05627614412975));
#8017=CARTESIAN_POINT('Ctrl Pts',(1.25309005838148,2.83577167184866,7.00389663962524));
#8018=CARTESIAN_POINT('Ctrl Pts',(2.16055854043283,2.22347081456344,6.95151713512074));
#8019=CARTESIAN_POINT('Ctrl Pts',(2.60876358347624,1.3699884259484,6.89913763061623));
#8020=CARTESIAN_POINT('Ctrl Pts',(3.05696862651966,0.516506037333356,6.84675812611173));
#8021=CARTESIAN_POINT('Ctrl Pts',(3.04591023055511,-0.578157882611513,6.79437862160723));
#8022=CARTESIAN_POINT('Ctrl Pts',(2.58055450279311,-1.42241139605186,6.74199911710272));
#8023=CARTESIAN_POINT('Ctrl Pts',(2.11519877503111,-2.26666490949219,6.68961961259822));
#8024=CARTESIAN_POINT('Ctrl Pts',(1.19554571547167,-2.86050801642801,6.63724010809371));
#8025=CARTESIAN_POINT('Ctrl Pts',(0.234593342362696,-2.93725751088208,6.5848606035892));
#8026=CARTESIAN_POINT('Ctrl Pts',(-0.726359030746288,-3.01400700533615,
6.5324810990847));
#8027=CARTESIAN_POINT('Ctrl Pts',(-1.72861071740481,-2.57366288730847,6.4801015945802));
#8028=CARTESIAN_POINT('Ctrl Pts',(-2.32207028787941,-1.813974999748,6.4277220900757));
#8029=CARTESIAN_POINT('Ctrl Pts',(-2.72068210106971,-1.30371182195979,6.39254009908033));
#8030=CARTESIAN_POINT('Ctrl Pts',(-2.93486858555413,-0.649377666932483,
6.35735810808496));
#8031=CARTESIAN_POINT('Ctrl Pts',(-2.93949980478958,0.00219056232359141,
6.3221761170896));
#8032=CARTESIAN_POINT('Ctrl Pts',(-2.94109090649655,0.00253660757586993,
6.1778238829104));
#8033=CARTESIAN_POINT('Ctrl Pts',(-2.9349800243151,-0.710047628629508,6.21635346422191));
#8034=CARTESIAN_POINT('Ctrl Pts',(-2.67397994955092,-1.42664569379386,6.25488304553342));
#8035=CARTESIAN_POINT('Ctrl Pts',(-2.20308134670334,-1.95680883878727,6.29341262684494));
#8036=CARTESIAN_POINT('Ctrl Pts',(-1.5621108005568,-2.67844818649031,6.34585773206864));
#8037=CARTESIAN_POINT('Ctrl Pts',(-0.532246708275948,-3.05466664015197,
6.39830283729235));
#8038=CARTESIAN_POINT('Ctrl Pts',(0.42295609402977,-2.91612352177857,6.45074794251606));
#8039=CARTESIAN_POINT('Ctrl Pts',(1.3781588963355,-2.77758040340517,6.50319304773977));
#8040=CARTESIAN_POINT('Ctrl Pts',(2.25870040866608,-2.12427571299673,6.55563815296348));
#8041=CARTESIAN_POINT('Ctrl Pts',(2.66823777423309,-1.25027014357196,6.60808325818718));
#8042=CARTESIAN_POINT('Ctrl Pts',(3.07777513980009,-0.376264574147203,6.66052836341089));
#8043=CARTESIAN_POINT('Ctrl Pts',(3.01630835860352,0.718441874293864,6.7129734686346));
#8044=CARTESIAN_POINT('Ctrl Pts',(2.51150440524776,1.54110800210975,6.76541857385831));
#8045=CARTESIAN_POINT('Ctrl Pts',(2.006700451892,2.36377412992563,6.81786367908202));
#8046=CARTESIAN_POINT('Ctrl Pts',(1.05855932637705,2.91439993711633,6.87030878430572));
#8047=CARTESIAN_POINT('Ctrl Pts',(0.0938513252260113,2.94514179293546,6.92275388952943));
#8048=CARTESIAN_POINT('Ctrl Pts',(-0.870856675925038,2.9758836487546,6.97519899475314));
#8049=CARTESIAN_POINT('Ctrl Pts',(-1.85213155271217,2.48674155320215,7.02764409997685));
#8050=CARTESIAN_POINT('Ctrl Pts',(-2.40828908863565,1.69788454181399,7.08008920520056));
#8051=CARTESIAN_POINT('Ctrl Pts',(-2.75376700818296,1.2078566962645,7.11266743110384));
#8052=CARTESIAN_POINT('Ctrl Pts',(-2.93520341737875,0.60217681128353,7.14524565700712));
#8053=CARTESIAN_POINT('Ctrl Pts',(-2.93846014819028,-0.00170708260597003,
7.1778238829104));
#8054=CARTESIAN_POINT('Origin',(0.,0.,0.));
#8055=CARTESIAN_POINT('',(-2.94622250669394,0.000937675328142526,8.3221761170896));
#8056=CARTESIAN_POINT('',(-2.94656696235233,-0.000396508504380587,8.1778238829104));
#8057=CARTESIAN_POINT('',(-2.942,-3.60291088309151E-16,0.));
#8058=CARTESIAN_POINT('Ctrl Pts',(-2.94622250669394,0.000937675328142526,
8.3221761170896));
#8059=CARTESIAN_POINT('Ctrl Pts',(-2.94645073222768,0.0548930361868928,
8.31924549547236));
#8060=CARTESIAN_POINT('Ctrl Pts',(-2.94509413407217,0.108836699779164,8.31631487385511));
#8061=CARTESIAN_POINT('Ctrl Pts',(-2.94211616003438,0.162690705921765,8.31338425223786));
#8062=CARTESIAN_POINT('Ctrl Pts',(-2.88889031756852,1.12523262560549,8.26100474773336));
#8063=CARTESIAN_POINT('Ctrl Pts',(-2.31771549444688,2.05913344782865,8.20862524322884));
#8064=CARTESIAN_POINT('Ctrl Pts',(-1.48509504480843,2.54499674522788,8.15624573872434));
#8065=CARTESIAN_POINT('Ctrl Pts',(-0.652474595169965,3.03086004262711,8.10386623421983));
#8066=CARTESIAN_POINT('Ctrl Pts',(0.44159148098532,3.06868581520241,8.05148672971533));
#8067=CARTESIAN_POINT('Ctrl Pts',(1.30577973958019,2.64148726651903,7.99910722521083));
#8068=CARTESIAN_POINT('Ctrl Pts',(2.16996799817506,2.21428871783565,7.94672772070633));
#8069=CARTESIAN_POINT('Ctrl Pts',(2.8042784392095,1.3220658478936,7.89434821620182));
#8070=CARTESIAN_POINT('Ctrl Pts',(2.92385476924452,0.36549831322338,7.84196871169732));
#8071=CARTESIAN_POINT('Ctrl Pts',(3.04343109927954,-0.591069221446826,7.78958920719281));
#8072=CARTESIAN_POINT('Ctrl Pts',(2.64827331831513,-1.61198142084519,7.73720970268831));
#8073=CARTESIAN_POINT('Ctrl Pts',(1.9158389819387,-2.23876678477201,7.68483019818381));
#8074=CARTESIAN_POINT('Ctrl Pts',(1.18340464556226,-2.86555214869884,7.6324506936793));
#8075=CARTESIAN_POINT('Ctrl Pts',(0.113693753773775,-3.09821067715411,7.58007118917479));
#8076=CARTESIAN_POINT('Ctrl Pts',(-0.812907669552306,-2.83226002346519,
7.52769168467029));
#8077=CARTESIAN_POINT('Ctrl Pts',(-1.73950909287838,-2.56630936977627,7.47531218016578));
#8078=CARTESIAN_POINT('Ctrl Pts',(-2.52300104774206,-1.80174953394315,7.42293267566128));
#8079=CARTESIAN_POINT('Ctrl Pts',(-2.81153277662714,-0.881929231056029,
7.37055317115678));
#8080=CARTESIAN_POINT('Ctrl Pts',(-2.90036087316611,-0.598751062127826,
7.35442748646772));
#8081=CARTESIAN_POINT('Ctrl Pts',(-2.94227697960606,-0.300857412821767,
7.33830180177866));
#8082=CARTESIAN_POINT('Ctrl Pts',(-2.93998607517527,-0.0023358300504342,
7.3221761170896));
#8083=CARTESIAN_POINT('Ctrl Pts',(-2.93846014819028,-0.00170708260597003,
7.1778238829104));
#8084=CARTESIAN_POINT('Ctrl Pts',(-2.94044617033292,-0.369968033311824,
7.19769076223082));
#8085=CARTESIAN_POINT('Ctrl Pts',(-2.87617048586605,-0.737561088352721,
7.21755764155125));
#8086=CARTESIAN_POINT('Ctrl Pts',(-2.7424268268773,-1.07785126568817,7.23742452087168));
#8087=CARTESIAN_POINT('Ctrl Pts',(-2.38936683413567,-1.97615813457835,7.28986962609539));
#8088=CARTESIAN_POINT('Ctrl Pts',(-1.55220665359259,-2.68419994513487,7.34231473131909));
#8089=CARTESIAN_POINT('Ctrl Pts',(-0.60776265660645,-2.88327813520494,7.3947598365428));
#8090=CARTESIAN_POINT('Ctrl Pts',(0.336681340379679,-3.082356325275,7.44720494176651));
#8091=CARTESIAN_POINT('Ctrl Pts',(1.38840915380886,-2.77247089485864,7.49965004699022));
#8092=CARTESIAN_POINT('Ctrl Pts',(2.07402481044015,-2.09310519028348,7.55209515221392));
#8093=CARTESIAN_POINT('Ctrl Pts',(2.75964046707144,-1.41373948570832,7.60454025743763));
#8094=CARTESIAN_POINT('Ctrl Pts',(3.07914396690482,-0.364893506974353,7.65698536266134));
#8095=CARTESIAN_POINT('Ctrl Pts',(2.8887227491853,0.5813339228528,7.70943046788505));
#8096=CARTESIAN_POINT('Ctrl Pts',(2.69830153146578,1.52756135267996,7.76187557310876));
#8097=CARTESIAN_POINT('Ctrl Pts',(1.99795559619334,2.37117023360031,7.81432067833246));
#8098=CARTESIAN_POINT('Ctrl Pts',(1.10291949457769,2.73244155291697,7.86676578355617));
#8099=CARTESIAN_POINT('Ctrl Pts',(0.207883392962048,3.09371287223363,7.91921088877988));
#8100=CARTESIAN_POINT('Ctrl Pts',(-0.881842874996807,2.97264662994661,7.97165599400359));
#8101=CARTESIAN_POINT('Ctrl Pts',(-1.67575975122609,2.42373627051487,8.0241010992273));
#8102=CARTESIAN_POINT('Ctrl Pts',(-2.45144772506959,1.88742928765845,8.07534202712166));
#8103=CARTESIAN_POINT('Ctrl Pts',(-2.94475435076587,0.942699847726619,8.12658295501603));
#8104=CARTESIAN_POINT('Ctrl Pts',(-2.94656696235233,-0.000396508504380587,
8.1778238829104));
#8105=CARTESIAN_POINT('Origin',(0.,0.,0.));
#8106=CARTESIAN_POINT('',(-2.93787859032851,0.00118007037484616,9.3221761170896));
#8107=CARTESIAN_POINT('',(-2.93938212312892,0.00216771032458683,9.1778238829104));
#8108=CARTESIAN_POINT('',(-2.942,-3.60291088309151E-16,0.));
#8109=CARTESIAN_POINT('Ctrl Pts',(-2.93787859032851,0.00118007037484616,
9.3221761170896));
#8110=CARTESIAN_POINT('Ctrl Pts',(-2.93938225399168,0.408942454113454,9.30018918916604));
#8111=CARTESIAN_POINT('Ctrl Pts',(-2.86009946358647,0.816145924853212,9.27820226124249));
#8112=CARTESIAN_POINT('Ctrl Pts',(-2.69715242952518,1.18654365111784,9.25621533331894));
#8113=CARTESIAN_POINT('Ctrl Pts',(-2.30896336853928,2.06894293121702,9.20383582881443));
#8114=CARTESIAN_POINT('Ctrl Pts',(-1.44594933104186,2.74245624053358,9.15145632430993));
#8115=CARTESIAN_POINT('Ctrl Pts',(-0.495674163844965,2.9046210644708,9.09907681980542));
#8116=CARTESIAN_POINT('Ctrl Pts',(0.454601003351916,3.06678588840801,9.04669731530092));
#8117=CARTESIAN_POINT('Ctrl Pts',(1.49213730024827,2.7176022269659,8.99431781079641));
#8118=CARTESIAN_POINT('Ctrl Pts',(2.15099835280526,2.01388208359571,8.94193830629191));
#8119=CARTESIAN_POINT('Ctrl Pts',(2.80985940536224,1.31016194022553,8.88955880178741));
#8120=CARTESIAN_POINT('Ctrl Pts',(3.09004521357986,0.251905314927287,8.8371792972829));
#8121=CARTESIAN_POINT('Ctrl Pts',(2.86572951288042,-0.685645923387644,8.7847997927784));
#8122=CARTESIAN_POINT('Ctrl Pts',(2.64141381218099,-1.62319716170258,8.73242028827389));
#8123=CARTESIAN_POINT('Ctrl Pts',(1.91259660256449,-2.44004301303419,8.68004078376939));
#8124=CARTESIAN_POINT('Ctrl Pts',(1.00657547791151,-2.76935400264746,8.62766127926488));
#8125=CARTESIAN_POINT('Ctrl Pts',(0.100554353258536,-3.09866499226073,8.57528177476038));
#8126=CARTESIAN_POINT('Ctrl Pts',(-0.982670686430926,-2.94044112015566,
8.52290227025587));
#8127=CARTESIAN_POINT('Ctrl Pts',(-1.75664477537062,-2.36573767553097,8.47052276575137));
#8128=CARTESIAN_POINT('Ctrl Pts',(-2.48731518632227,-1.82318876070292,8.42107388286411));
#8129=CARTESIAN_POINT('Ctrl Pts',(-2.94237161798714,-0.909460413780999,
8.37162499997686));
#8130=CARTESIAN_POINT('Ctrl Pts',(-2.94622250669394,0.000937675328142526,
8.3221761170896));
#8131=CARTESIAN_POINT('Ctrl Pts',(-2.94656696235233,-0.000396508504380587,
8.1778238829104));
#8132=CARTESIAN_POINT('Ctrl Pts',(-2.94660955927376,-0.0225595585939061,
8.17902806023974));
#8133=CARTESIAN_POINT('Ctrl Pts',(-2.94638072162746,-0.0447217067897041,
8.18023223756908));
#8134=CARTESIAN_POINT('Ctrl Pts',(-2.94587773547044,-0.0668776312364038,
8.18143641489842));
#8135=CARTESIAN_POINT('Ctrl Pts',(-2.92397135898579,-1.03182669697942,8.23388152012213));
#8136=CARTESIAN_POINT('Ctrl Pts',(-2.3820511215168,-1.98497035188899,8.28632662534583));
#8137=CARTESIAN_POINT('Ctrl Pts',(-1.5640421648278,-2.49728659914907,8.33877173056954));
#8138=CARTESIAN_POINT('Ctrl Pts',(-0.746033208138801,-3.00960284640916,
8.39121683579325));
#8139=CARTESIAN_POINT('Ctrl Pts',(0.348064467770205,-3.08109168601973,8.44366194101695));
#8140=CARTESIAN_POINT('Ctrl Pts',(1.22578367546087,-2.6795750856597,8.49610704624066));
#8141=CARTESIAN_POINT('Ctrl Pts',(2.10350288315153,-2.27805848529968,8.54855215146437));
#8142=CARTESIAN_POINT('Ctrl Pts',(2.76484362262384,-1.40353644496905,8.60099725668809));
#8143=CARTESIAN_POINT('Ctrl Pts',(2.91212808132915,-0.44964238612263,8.65344236191179));
#8144=CARTESIAN_POINT('Ctrl Pts',(3.05941254003446,0.504251672723784,8.7058874671355));
#8145=CARTESIAN_POINT('Ctrl Pts',(2.69264071797276,1.537517750086,8.75833257235921));
#8146=CARTESIAN_POINT('Ctrl Pts',(1.97690123029279,2.18506974304829,8.81077767758291));
#8147=CARTESIAN_POINT('Ctrl Pts',(1.26116174261282,2.83262173601059,8.86322278280662));
#8148=CARTESIAN_POINT('Ctrl Pts',(0.196454589314577,3.09445964457298,8.91566788803033));
#8149=CARTESIAN_POINT('Ctrl Pts',(-0.737982063629216,2.8527269003752,8.96811299325404));
#8150=CARTESIAN_POINT('Ctrl Pts',(-1.672418716573,2.61099415617743,9.02055809847774));
#8151=CARTESIAN_POINT('Ctrl Pts',(-2.47658486916233,1.86569075921951,9.07300320370145));
#8152=CARTESIAN_POINT('Ctrl Pts',(-2.78851523225651,0.952287217651892,9.12544830892515));
#8153=CARTESIAN_POINT('Ctrl Pts',(-2.89235416848512,0.648223031136026,9.1429068335869));
#8154=CARTESIAN_POINT('Ctrl Pts',(-2.94164516567622,0.325530543639097,9.16036535824865));
#8155=CARTESIAN_POINT('Ctrl Pts',(-2.93938212312892,0.00216771032458683,
9.1778238829104));
#8156=CARTESIAN_POINT('Origin',(0.,0.,0.));
#8157=CARTESIAN_POINT('',(-2.94242444587263,-0.00248500551853048,10.3221761170896));
#8158=CARTESIAN_POINT('',(-2.93989309841074,-0.00232834448912937,10.1778238829104));
#8159=CARTESIAN_POINT('',(-2.942,-3.60291088309151E-16,0.));
#8160=CARTESIAN_POINT('Ctrl Pts',(-2.94242444587263,-0.00248500551853048,
10.3221761170896));
#8161=CARTESIAN_POINT('Ctrl Pts',(-2.93565996783783,0.755676872330999,10.2811328828597));
#8162=CARTESIAN_POINT('Ctrl Pts',(-2.63573211439715,1.5185652175411,10.2400896486299));
#8163=CARTESIAN_POINT('Ctrl Pts',(-2.10792737213773,2.05892622612073,10.1990464144));
#8164=CARTESIAN_POINT('Ctrl Pts',(-1.43434130141424,2.74853664338077,10.1466669098955));
#8165=CARTESIAN_POINT('Ctrl Pts',(-0.389613404070186,3.07571802003838,10.094287405391));
#8166=CARTESIAN_POINT('Ctrl Pts',(0.557026464387836,2.89349108573471,10.0419079008865));
#8167=CARTESIAN_POINT('Ctrl Pts',(1.50366633284582,2.71126415143105,9.98952839638201));
#8168=CARTESIAN_POINT('Ctrl Pts',(2.35221817241779,2.01962890616612,9.9371488918775));
#8169=CARTESIAN_POINT('Ctrl Pts',(2.72164717416933,1.12921048240304,9.884769387373));
#8170=CARTESIAN_POINT('Ctrl Pts',(3.09107617592089,0.238792058639911,9.83238988286849));
#8171=CARTESIAN_POINT('Ctrl Pts',(2.981382339852,-0.85040954362138,9.78001037836398));
#8172=CARTESIAN_POINT('Ctrl Pts',(2.44180970997212,-1.64926869616342,9.72763087385948));
#8173=CARTESIAN_POINT('Ctrl Pts',(1.90223708009224,-2.44812784870545,9.67525136935497));
#8174=CARTESIAN_POINT('Ctrl Pts',(0.93278565640137,-2.95664455152821,9.62287186485046));
#8175=CARTESIAN_POINT('Ctrl Pts',(-0.031174037472469,-2.94644704900523,
9.57049236034596));
#8176=CARTESIAN_POINT('Ctrl Pts',(-0.995133731346301,-2.93624954648225,
9.51811285584146));
#8177=CARTESIAN_POINT('Ctrl Pts',(-1.9536016954031,-2.40733783861356,9.46573335133695));
#8178=CARTESIAN_POINT('Ctrl Pts',(-2.4761536351943,-1.5972393592383,9.41335384683245));
#8179=CARTESIAN_POINT('Ctrl Pts',(-2.77935810415337,-1.1271894741653,9.3829612702515));
#8180=CARTESIAN_POINT('Ctrl Pts',(-2.93580007289335,-0.56247072784923,9.35256869367055));
#8181=CARTESIAN_POINT('Ctrl Pts',(-2.93787859032851,0.00118007037484616,
9.3221761170896));
#8182=CARTESIAN_POINT('Ctrl Pts',(-2.93938212312892,0.00216771032458683,
9.1778238829104));
#8183=CARTESIAN_POINT('Ctrl Pts',(-2.93484702512206,-0.645845798130107,
9.21281046347236));
#8184=CARTESIAN_POINT('Ctrl Pts',(-2.72327366311651,-1.29655137950586,9.24779704403432));
#8185=CARTESIAN_POINT('Ctrl Pts',(-2.32875660055073,-1.80542543875765,9.28278362459629));
#8186=CARTESIAN_POINT('Ctrl Pts',(-1.73737303215174,-2.56823086742229,9.33522872981999));
#8187=CARTESIAN_POINT('Ctrl Pts',(-0.73491132175476,-3.01233803857425,9.3876738350437));
#8188=CARTESIAN_POINT('Ctrl Pts',(0.227407657021308,-2.93784857599215,9.44011894026741));
#8189=CARTESIAN_POINT('Ctrl Pts',(1.1897266357974,-2.86335911341005,9.49256404549111));
#8190=CARTESIAN_POINT('Ctrl Pts',(2.11190288295256,-2.27027301709385,9.54500915071482));
#8191=CARTESIAN_POINT('Ctrl Pts',(2.57885359588429,-1.42554607687093,9.59745425593853));
#8192=CARTESIAN_POINT('Ctrl Pts',(3.045804308816,-0.580819136648041,9.64989936116224));
#8193=CARTESIAN_POINT('Ctrl Pts',(3.05752948752431,0.515548647481566,9.70234446638595));
#8194=CARTESIAN_POINT('Ctrl Pts',(2.60875076544854,1.37006875926759,9.75478957160966));
#8195=CARTESIAN_POINT('Ctrl Pts',(2.15997204337277,2.22458887105361,9.80723467683336));
#8196=CARTESIAN_POINT('Ctrl Pts',(1.25068942051291,2.83726131049606,9.85967978205706));
#8197=CARTESIAN_POINT('Ctrl Pts',(0.290183858659324,2.93231357229399,9.91212488728077));
#8198=CARTESIAN_POINT('Ctrl Pts',(-0.67032170319427,3.02736583409193,9.96456999250448));
#8199=CARTESIAN_POINT('Ctrl Pts',(-1.68205020404159,2.60479791824536,10.0170150977282));
#8200=CARTESIAN_POINT('Ctrl Pts',(-2.28961248249041,1.85481470515708,10.0694602029519));
#8201=CARTESIAN_POINT('Ctrl Pts',(-2.708067067946,1.33826862311137,10.1055814296047));
#8202=CARTESIAN_POINT('Ctrl Pts',(-2.93479827488144,0.666407318052135,10.1417026562576));
#8203=CARTESIAN_POINT('Ctrl Pts',(-2.93989309841074,-0.00232834448912937,
10.1778238829104));
#8204=CARTESIAN_POINT('Origin',(0.,0.,-1.84858989190501));
#8205=CARTESIAN_POINT('',(-2.3720921752204,-0.00200333509135781,10.651410108095));
#8206=CARTESIAN_POINT('',(-2.37533330856671,0.000645282184899808,10.848589891905));
#8207=CARTESIAN_POINT('',(-2.37175,-1.78696459712734E-13,-1.84858989190501));
#8208=CARTESIAN_POINT('',(-2.34668236863852,0.343918483395543,11.62825));
#8209=CARTESIAN_POINT('Ctrl Pts',(-2.3720921752204,-0.00200333509135741,
10.651410108095));
#8210=CARTESIAN_POINT('Ctrl Pts',(-2.37359839777753,-0.170820576644891,
10.6627463783696));
#8211=CARTESIAN_POINT('Ctrl Pts',(-2.28072670946568,-1.11802807678178,10.7264621531488));
#8212=CARTESIAN_POINT('Ctrl Pts',(-1.0098707589218,-2.60498459805753,10.8425574324324));
#8213=CARTESIAN_POINT('Ctrl Pts',(1.61803174729613,-2.2773674076414,10.999695945946));
#8214=CARTESIAN_POINT('Ctrl Pts',(2.79127527466209,0.0946110570183949,11.1568344594594));
#8215=CARTESIAN_POINT('Ctrl Pts',(1.46022534703361,2.38369320998594,11.313972972973));
#8216=CARTESIAN_POINT('Ctrl Pts',(-1.1878082887304,2.52773050943662,11.4711114864865));
#8217=CARTESIAN_POINT('Ctrl Pts',(-2.23349531079268,1.11623543008163,11.5758704954955));
#8218=CARTESIAN_POINT('Ctrl Pts',(-2.34668236863853,0.343918483395475,11.62825));
#8219=CARTESIAN_POINT('',(-0.439445221994028,2.33068358199191,11.62825));
#8220=CARTESIAN_POINT('Origin',(0.,0.,11.62825));
#8221=CARTESIAN_POINT('Ctrl Pts',(-2.37533330856671,0.000645282184899929,
10.848589891905));
#8222=CARTESIAN_POINT('Ctrl Pts',(-2.37266626526946,-0.74297942345447,10.8986961737085));
#8223=CARTESIAN_POINT('Ctrl Pts',(-1.5987407489101,-2.26979394046941,11.0012475607357));
#8224=CARTESIAN_POINT('Ctrl Pts',(0.989622905930635,-2.61290295808564,11.1562440529866));
#8225=CARTESIAN_POINT('Ctrl Pts',(2.72902843688469,-0.61088887604173,11.3135793686578));
#8226=CARTESIAN_POINT('Ctrl Pts',(2.00599839187704,1.9449087769569,11.4709146843289));
#8227=CARTESIAN_POINT('Ctrl Pts',(0.328567026486064,2.47549058867235,11.5758048947763));
#8228=CARTESIAN_POINT('Ctrl Pts',(-0.439445221994061,2.3306835819919,11.62825));
#8229=CARTESIAN_POINT('Origin',(0.,0.,-1.84858989190501));
#8230=CARTESIAN_POINT('',(-2.36842744616303,0.000951336475574988,9.65141010809499));
#8231=CARTESIAN_POINT('',(-2.37005148067835,-0.00187703978340947,9.84858989190503));
#8232=CARTESIAN_POINT('',(-2.37175,-1.78696459712734E-13,-1.84858989190501));
#8233=CARTESIAN_POINT('Ctrl Pts',(-2.36842744616303,0.000951336475575049,
9.65141010809499));
#8234=CARTESIAN_POINT('Ctrl Pts',(-2.36675180927421,-0.453446617531184,
9.68180268467594));
#8235=CARTESIAN_POINT('Ctrl Pts',(-2.02327622703562,-1.69331275929724,9.76457476576139));
#8236=CARTESIAN_POINT('Ctrl Pts',(-0.0295588149451427,-2.79350652787453,
9.89972635135136));
#8237=CARTESIAN_POINT('Ctrl Pts',(2.31506703223917,-1.56365490661018,10.0568648648649));
#8238=CARTESIAN_POINT('Ctrl Pts',(2.58036243233743,1.07058768363104,10.2140033783784));
#8239=CARTESIAN_POINT('Ctrl Pts',(0.528133174514654,2.74331293137788,10.3711418918919));
#8240=CARTESIAN_POINT('Ctrl Pts',(-1.81626974066498,2.00910742659655,10.5169441351307));
#8241=CARTESIAN_POINT('Ctrl Pts',(-2.36663886088356,0.609203474490441,10.6103668738651));
#8242=CARTESIAN_POINT('Ctrl Pts',(-2.3720921752204,-0.00200333509135741,
10.651410108095));
#8243=CARTESIAN_POINT('Ctrl Pts',(-2.37005148067835,-0.0018770397834093,
9.84858989190503));
#8244=CARTESIAN_POINT('Ctrl Pts',(-2.37190764427919,-0.245513112411714,
9.8649137704759));
#8245=CARTESIAN_POINT('Ctrl Pts',(-2.22599738542921,-1.26973141402768,9.93368275427047));
#8246=CARTESIAN_POINT('Ctrl Pts',(-0.757654725048104,-2.69016151139635,
10.0548968432888));
#8247=CARTESIAN_POINT('Ctrl Pts',(1.83027666927001,-2.11210170665972,10.2122321589599));
#8248=CARTESIAN_POINT('Ctrl Pts',(2.77060484795253,0.367287133540841,10.369567474631));
#8249=CARTESIAN_POINT('Ctrl Pts',(1.21665350181368,2.51610800548609,10.5269027903021));
#8250=CARTESIAN_POINT('Ctrl Pts',(-1.43234772356642,2.39972494583597,10.6842381059733));
#8251=CARTESIAN_POINT('Ctrl Pts',(-2.35921176770024,0.848280000432971,10.7914671398409));
#8252=CARTESIAN_POINT('Ctrl Pts',(-2.37545779881228,0.0353556381482985,
10.8462510684848));
#8253=CARTESIAN_POINT('Ctrl Pts',(-2.37533330856671,0.000645282184899929,
10.848589891905));
#8254=CARTESIAN_POINT('Origin',(0.,0.,-1.84858989190501));
#8255=CARTESIAN_POINT('',(-2.37515405515002,0.000755925037124906,8.65141010809499));
#8256=CARTESIAN_POINT('',(-2.36963954810708,0.00174754145538428,8.84858989190503));
#8257=CARTESIAN_POINT('',(-2.37175,-1.78696459712734E-13,-1.84858989190501));
#8258=CARTESIAN_POINT('Ctrl Pts',(-2.37515405515002,0.00075592503712492,
8.65141010809499));
#8259=CARTESIAN_POINT('Ctrl Pts',(-2.37204958700235,-0.733179040239741,
8.70085899098224));
#8260=CARTESIAN_POINT('Ctrl Pts',(-1.61660279875904,-2.25007474146859,8.80268737837401));
#8261=CARTESIAN_POINT('Ctrl Pts',(0.954326572136137,-2.62560372673677,8.95689527027026));
#8262=CARTESIAN_POINT('Ctrl Pts',(2.71697669134881,-0.650055649344734,9.11403378378378));
#8263=CARTESIAN_POINT('Ctrl Pts',(2.03934512373477,1.90934627218937,9.2711722972973));
#8264=CARTESIAN_POINT('Ctrl Pts',(-0.469944521571767,2.75384968723896,9.42831081081079));
#8265=CARTESIAN_POINT('Ctrl Pts',(-2.15345863304216,1.44000181080629,9.55505674774338));
#8266=CARTESIAN_POINT('Ctrl Pts',(-2.36963965360463,0.329676840769313,9.62942318017144));
#8267=CARTESIAN_POINT('Ctrl Pts',(-2.36842744616303,0.000951336475575049,
9.65141010809499));
#8268=CARTESIAN_POINT('Ctrl Pts',(-2.36963954810708,0.00174754145538407,
8.84858989190503));
#8269=CARTESIAN_POINT('Ctrl Pts',(-2.36598349144566,-0.520661037292834,
8.88357647246699));
#8270=CARTESIAN_POINT('Ctrl Pts',(-1.9397431197991,-1.83158688452099,8.97100815825266));
#8271=CARTESIAN_POINT('Ctrl Pts',(0.215690902196592,-2.78647992051942,9.11088494926201));
#8272=CARTESIAN_POINT('Ctrl Pts',(2.4459813653409,-1.35209655994371,9.26822026493315));
#8273=CARTESIAN_POINT('Ctrl Pts',(2.47433880171217,1.29947749716991,9.42555558060427));
#8274=CARTESIAN_POINT('Ctrl Pts',(0.275231669725872,2.78123058171878,9.58289089627539));
#8275=CARTESIAN_POINT('Ctrl Pts',(-1.91777323438188,1.86527979947427,9.72390233337565));
#8276=CARTESIAN_POINT('Ctrl Pts',(-2.36594419049973,0.537237102851684,9.81246866525219));
#8277=CARTESIAN_POINT('Ctrl Pts',(-2.37005148067835,-0.0018770397834093,
9.84858989190503));
#8278=CARTESIAN_POINT('Origin',(0.,0.,-1.84858989190501));
#8279=CARTESIAN_POINT('',(-2.37012643568897,-0.00188307441280249,7.65141010809499));
#8280=CARTESIAN_POINT('',(-2.37543174471759,-0.000319652972777529,7.84858989190503));
#8281=CARTESIAN_POINT('',(-2.37175,-1.78696459712734E-13,-1.84858989190501));
#8282=CARTESIAN_POINT('Ctrl Pts',(-2.37012643568897,-0.00188307441280247,
7.65141010809499));
#8283=CARTESIAN_POINT('Ctrl Pts',(-2.37197329244753,-0.242542001652036,
7.66753579278404));
#8284=CARTESIAN_POINT('Ctrl Pts',(-2.22842022339473,-1.26275955622086,7.7360409819776));
#8285=CARTESIAN_POINT('Ctrl Pts',(-0.770711640749916,-2.68524440462409,
7.85692567567567));
#8286=CARTESIAN_POINT('Ctrl Pts',(1.81639251383808,-2.12255793467458,8.01406418918919));
#8287=CARTESIAN_POINT('Ctrl Pts',(2.77208469636934,0.346526200869026,8.1712027027027));
#8288=CARTESIAN_POINT('Ctrl Pts',(1.23799993580832,2.50437418705365,8.32834121621622));
#8289=CARTESIAN_POINT('Ctrl Pts',(-1.40800742257503,2.4128922603655,8.48547972972973));
#8290=CARTESIAN_POINT('Ctrl Pts',(-2.35469744140074,0.865004378788607,8.59316936035599));
#8291=CARTESIAN_POINT('Ctrl Pts',(-2.37533804356255,0.0442530790537146,
8.64847948647774));
#8292=CARTESIAN_POINT('Ctrl Pts',(-2.37515405515002,0.00075592503712492,
8.65141010809499));
#8293=CARTESIAN_POINT('Ctrl Pts',(-2.37543174471759,-0.000319652972777509,
7.84858989190503));
#8294=CARTESIAN_POINT('Ctrl Pts',(-2.37546608504675,-0.0181868229420618,
7.84979406923436));
#8295=CARTESIAN_POINT('Ctrl Pts',(-2.36724692977477,-0.814184073087101,
7.9034433517874));
#8296=CARTESIAN_POINT('Ctrl Pts',(-1.48345697628832,-2.36861723168749,8.00953773956416));
#8297=CARTESIAN_POINT('Ctrl Pts',(1.16262680634646,-2.54151354917186,8.16687305523529));
#8298=CARTESIAN_POINT('Ctrl Pts',(2.76208455499713,-0.426475157784177,8.3242083709064));
#8299=CARTESIAN_POINT('Ctrl Pts',(1.8750440359881,2.07248692819523,8.48154368657753));
#8300=CARTESIAN_POINT('Ctrl Pts',(-0.699958537943023,2.7057439570526,8.63887900224866));
#8301=CARTESIAN_POINT('Ctrl Pts',(-2.21235813584821,1.30404785948979,8.76122773735781));
#8302=CARTESIAN_POINT('Ctrl Pts',(-2.37146394347132,0.262432721575661,8.83113136724327));
#8303=CARTESIAN_POINT('Ctrl Pts',(-2.36963954810708,0.00174754145538407,
8.84858989190503));
#8304=CARTESIAN_POINT('Origin',(0.,0.,-1.84858989190501));
#8305=CARTESIAN_POINT('',(-2.36973441944585,0.0017659640348839,6.65141010809499));
#8306=CARTESIAN_POINT('',(-2.36889628024144,-0.00137619754296547,6.84858989190503));
#8307=CARTESIAN_POINT('',(-2.37175,-1.78696459712734E-13,-1.84858989190501));
#8308=CARTESIAN_POINT('Ctrl Pts',(-2.36973441944585,0.00176596403488379,
6.65141010809499));
#8309=CARTESIAN_POINT('Ctrl Pts',(-2.36600087280351,-0.523508321396127,
6.68659209909035));
#8310=CARTESIAN_POINT('Ctrl Pts',(-1.93625564677593,-1.83636884117464,6.77415359459022));
#8311=CARTESIAN_POINT('Ctrl Pts',(0.222416181733502,-2.78479173243988,6.91409459459459));
#8312=CARTESIAN_POINT('Ctrl Pts',(2.4466042959518,-1.34857753576241,7.0712331081081));
#8313=CARTESIAN_POINT('Ctrl Pts',(2.47334911304448,1.29887571249989,7.22837162162162));
#8314=CARTESIAN_POINT('Ctrl Pts',(0.278629494786153,2.77973012269657,7.38551013513513));
#8315=CARTESIAN_POINT('Ctrl Pts',(-1.91543890246215,1.86818192765693,7.52652296395959));
#8316=CARTESIAN_POINT('Ctrl Pts',(-2.36597432596829,0.539167154048567,7.61515628827954));
#8317=CARTESIAN_POINT('Ctrl Pts',(-2.37012643568897,-0.00188307441280247,
7.65141010809499));
#8318=CARTESIAN_POINT('Ctrl Pts',(-2.36889628024144,-0.0013761975429653,
6.84858989190503));
#8319=CARTESIAN_POINT('Ctrl Pts',(-2.37049735026751,-0.298256860301772,
6.86845677122545));
#8320=CARTESIAN_POINT('Ctrl Pts',(-2.18189218700624,-1.37689100842058,6.94076875576958));
#8321=CARTESIAN_POINT('Ctrl Pts',(-0.57644849505612,-2.73472106868152,7.06552584553741));
#8322=CARTESIAN_POINT('Ctrl Pts',(1.96716344393165,-1.98526073259378,7.22286116120855));
#8323=CARTESIAN_POINT('Ctrl Pts',(2.73988515609665,0.551381466653972,7.38019647687966));
#8324=CARTESIAN_POINT('Ctrl Pts',(1.04609303646807,2.5916561403346,7.53753179255079));
#8325=CARTESIAN_POINT('Ctrl Pts',(-1.56924738212969,2.3010974504224,7.69366293089257));
#8326=CARTESIAN_POINT('Ctrl Pts',(-2.3739704729535,0.759975650525201,7.79734896401065));
#8327=CARTESIAN_POINT('Ctrl Pts',(-2.37543174471759,-0.000319652972777509,
7.84858989190503));
#8328=CARTESIAN_POINT('Origin',(0.,0.,-1.84858989190501));
#8329=CARTESIAN_POINT('',(-2.37533640146812,-0.000487534612837604,5.65141010809499));
#8330=CARTESIAN_POINT('',(-2.3710171167516,0.00204493508413422,5.84858989190502));
#8331=CARTESIAN_POINT('',(-2.37175,-1.78696459712734E-13,-1.84858989190501));
#8332=CARTESIAN_POINT('Ctrl Pts',(-2.37533640146812,-0.000487534612837498,
5.65141010809499));
#8333=CARTESIAN_POINT('Ctrl Pts',(-2.3754150982357,-0.0280706202968775,
5.65326890089215));
#8334=CARTESIAN_POINT('Ctrl Pts',(-2.36258260410634,-0.832851216236821,
5.70750719819383));
#8335=CARTESIAN_POINT('Ctrl Pts',(-1.45646562934828,-2.38395507960311,5.81412499999999));
#8336=CARTESIAN_POINT('Ctrl Pts',(1.18715361157964,-2.5288733170224,5.97126351351352));
#8337=CARTESIAN_POINT('Ctrl Pts',(2.76451839080433,-0.402457473451116,6.12840202702702));
#8338=CARTESIAN_POINT('Ctrl Pts',(1.8589019956498,2.08542976904401,6.28554054054054));
#8339=CARTESIAN_POINT('Ctrl Pts',(-0.716306714602523,2.70026640197657,6.44267905405405));
#8340=CARTESIAN_POINT('Ctrl Pts',(-2.21563200675447,1.29517183256302,6.5646355765722));
#8341=CARTESIAN_POINT('Ctrl Pts',(-2.37155943608083,0.258528340584143,6.63421259458585));
#8342=CARTESIAN_POINT('Ctrl Pts',(-2.36973441944585,0.00176596403488379,
6.65141010809499));
#8343=CARTESIAN_POINT('Ctrl Pts',(-2.3710171167516,0.00204493508413416,
5.84858989190502));
#8344=CARTESIAN_POINT('Ctrl Pts',(-2.36609071130836,-0.572418580286349,
5.88711947321653));
#8345=CARTESIAN_POINT('Ctrl Pts',(-1.86927748327345,-1.93646185988882,5.97809415975175));
#8346=CARTESIAN_POINT('Ctrl Pts',(0.401163844498212,-2.76587414046649,6.12151395151068));
#8347=CARTESIAN_POINT('Ctrl Pts',(2.53076037597685,-1.18585163930103,6.2788492671818));
#8348=CARTESIAN_POINT('Ctrl Pts',(2.38210248511723,1.46170446446183,6.43618458285292));
#8349=CARTESIAN_POINT('Ctrl Pts',(0.0890157606711408,2.793397283841,6.59351989852405));
#8350=CARTESIAN_POINT('Ctrl Pts',(-1.98453634187054,1.75978107224967,6.73098833487474));
#8351=CARTESIAN_POINT('Ctrl Pts',(-2.36627080393209,0.485456441931073,6.81601166600174));
#8352=CARTESIAN_POINT('Ctrl Pts',(-2.36889628024144,-0.0013761975429653,
6.84858989190503));
#8353=CARTESIAN_POINT('Origin',(0.,0.,-1.84858989190501));
#8354=CARTESIAN_POINT('',(-2.36864740940268,-0.0011676470311218,4.65141010809498));
#8355=CARTESIAN_POINT('',(-2.37471653528189,-0.00117837014130401,4.84858989190502));
#8356=CARTESIAN_POINT('',(-2.37175,-1.78696459712734E-13,-1.84858989190501));
#8357=CARTESIAN_POINT('Ctrl Pts',(-2.36864740940268,-0.00116764703112199,
4.65141010809498));
#8358=CARTESIAN_POINT('Ctrl Pts',(-2.37007090104248,-0.313795660845675,
4.67232520719846));
#8359=CARTESIAN_POINT('Ctrl Pts',(-2.16810014725707,-1.40760004764448,4.74561981080643));
#8360=CARTESIAN_POINT('Ctrl Pts',(-0.525482821607704,-2.74379331497496,
4.87129391891892));
#8361=CARTESIAN_POINT('Ctrl Pts',(2.00035639160479,-1.95015595724574,5.02843243243243));
#8362=CARTESIAN_POINT('Ctrl Pts',(2.72955454106374,0.595034417816705,5.18557094594594));
#8363=CARTESIAN_POINT('Ctrl Pts',(1.0071746643292,2.60578839251754,5.34270945945947));
#8364=CARTESIAN_POINT('Ctrl Pts',(-1.58873507575841,2.28002578161798,5.49798918017579));
#8365=CARTESIAN_POINT('Ctrl Pts',(-2.37319747737008,0.7492017916888,5.60088939638765));
#8366=CARTESIAN_POINT('Ctrl Pts',(-2.37533640146812,-0.000487534612837498,
5.65141010809499));
#8367=CARTESIAN_POINT('Ctrl Pts',(-2.37471653528189,-0.00117837014130423,
4.84858989190502));
#8368=CARTESIAN_POINT('Ctrl Pts',(-2.37515017179056,-0.0716719020310164,
4.85333706998391));
#8369=CARTESIAN_POINT('Ctrl Pts',(-2.34054813360425,-0.920521113001663,
4.91052935328651));
#8370=CARTESIAN_POINT('Ctrl Pts',(-1.32208186928512,-2.46233460804071,5.02016674181281));
#8371=CARTESIAN_POINT('Ctrl Pts',(1.32964132424929,-2.45826079574207,5.17750205748394));
#8372=CARTESIAN_POINT('Ctrl Pts',(2.78438780839412,-0.241198514719961,5.33483737315506));
#8373=CARTESIAN_POINT('Ctrl Pts',(1.73255804842731,2.19299676239354,5.49217268882618));
#8374=CARTESIAN_POINT('Ctrl Pts',(-0.878964234485193,2.65300095467984,5.64950800449731));
#8375=CARTESIAN_POINT('Ctrl Pts',(-2.25346115704322,1.19692341827648,5.76831373885692));
#8376=CARTESIAN_POINT('Ctrl Pts',(-2.37279636039799,0.20952086689332,5.83467436799283));
#8377=CARTESIAN_POINT('Ctrl Pts',(-2.3710171167516,0.00204493508413416,
5.84858989190502));
#8378=CARTESIAN_POINT('Origin',(0.,0.,-1.84858989190501));
#8379=CARTESIAN_POINT('',(-2.37165914320747,0.00205379600805495,3.65141010809498));
#8380=CARTESIAN_POINT('',(-2.36819322153198,-0.000653453332863235,3.84858989190502));
#8381=CARTESIAN_POINT('',(-2.37175,-1.78696459712734E-13,-1.84858989190501));
#8382=CARTESIAN_POINT('Ctrl Pts',(-2.37165914320747,0.0020537960080548,
3.65141010809498));
#8383=CARTESIAN_POINT('Ctrl Pts',(-2.36638740749304,-0.593495286532831,
3.69138151350476));
#8384=CARTESIAN_POINT('Ctrl Pts',(-1.83931642681201,-1.97778866762885,3.78373242341905));
#8385=CARTESIAN_POINT('Ctrl Pts',(0.47257542983782,-2.75339906613161,3.92846283783783));
#8386=CARTESIAN_POINT('Ctrl Pts',(2.55822296043148,-1.12251023841371,4.08560135135135));
#8387=CARTESIAN_POINT('Ctrl Pts',(2.34617571991457,1.51657292659299,4.24273986486486));
#8388=CARTESIAN_POINT('Ctrl Pts',(0.0268861606557786,2.79353021925399,4.39987837837838));
#8389=CARTESIAN_POINT('Ctrl Pts',(-2.00464048744226,1.72543877128143,4.53610179278842));
#8390=CARTESIAN_POINT('Ctrl Pts',(-2.36650592693501,0.469145905762286,4.61994570269395));
#8391=CARTESIAN_POINT('Ctrl Pts',(-2.36864740940268,-0.00116764703112199,
4.65141010809498));
#8392=CARTESIAN_POINT('Ctrl Pts',(-2.36819322153198,-0.000653453332863235,
3.84858989190502));
#8393=CARTESIAN_POINT('Ctrl Pts',(-2.36907284142701,-0.350739660290616,
3.871999771975));
#8394=CARTESIAN_POINT('Ctrl Pts',(-2.13320735842129,-1.48399610964751,3.94785475726868));
#8395=CARTESIAN_POINT('Ctrl Pts',(-0.392663608746353,-2.76709368867159,
4.07615484778607));
#8396=CARTESIAN_POINT('Ctrl Pts',(2.09526330020315,-1.8495577562663,4.23349016345719));
#8397=CARTESIAN_POINT('Ctrl Pts',(2.69698125586998,0.732996791565816,4.39082547912832));
#8398=CARTESIAN_POINT('Ctrl Pts',(0.870808554093777,2.65568911080063,4.54816079479944));
#8399=CARTESIAN_POINT('Ctrl Pts',(-1.66053522846232,2.20178445767042,4.70074893239168));
#8400=CARTESIAN_POINT('Ctrl Pts',(-2.37035951259304,0.707115123883991,4.8008919647602));
#8401=CARTESIAN_POINT('Ctrl Pts',(-2.37471653528189,-0.00117837014130423,
4.84858989190502));
#8402=CARTESIAN_POINT('Origin',(0.,0.,-1.84858989190501));
#8403=CARTESIAN_POINT('',(-2.37406517885066,-0.00153607482357252,2.65141010809498));
#8404=CARTESIAN_POINT('',(-2.37255724078598,0.00199178475905649,2.84858989190502));
#8405=CARTESIAN_POINT('',(-2.37175,-1.78696459712734E-13,-1.84858989190501));
#8406=CARTESIAN_POINT('Ctrl Pts',(-2.37406517885066,-0.00153607482357281,
2.65141010809498));
#8407=CARTESIAN_POINT('Ctrl Pts',(-2.37481281249436,-0.100330398866114,
2.65805831530656));
#8408=CARTESIAN_POINT('Ctrl Pts',(-2.32469515905834,-0.976735840432517,
2.71708602702265));
#8409=CARTESIAN_POINT('Ctrl Pts',(-1.23560715428754,-2.50555554774625,2.82849324324324));
#8410=CARTESIAN_POINT('Ctrl Pts',(1.41031161531747,-2.41154623133624,2.98563175675675));
#8411=CARTESIAN_POINT('Ctrl Pts',(2.78954424185296,-0.151581281506301,3.14277027027027));
#8412=CARTESIAN_POINT('Ctrl Pts',(1.66331845351111,2.24452793077997,3.29990878378378));
#8413=CARTESIAN_POINT('Ctrl Pts',(-0.956834235921451,2.62469088021855,3.45704729729729));
#8414=CARTESIAN_POINT('Ctrl Pts',(-2.26971028444252,1.15040938517441,3.57421440540103));
#8415=CARTESIAN_POINT('Ctrl Pts',(-2.37329561854466,0.186926755969883,3.63900200900026));
#8416=CARTESIAN_POINT('Ctrl Pts',(-2.37165914320747,0.0020537960080548,
3.65141010809498));
#8417=CARTESIAN_POINT('Ctrl Pts',(-2.37255724078598,0.00199178475905658,
2.84858989190502));
#8418=CARTESIAN_POINT('Ctrl Pts',(-2.36697397570993,-0.624252704055323,
2.89066247396608));
#8419=CARTESIAN_POINT('Ctrl Pts',(-1.79321255273579,-2.04018921676783,2.98518016125086));
#8420=CARTESIAN_POINT('Ctrl Pts',(0.584848394656438,-2.73293698550247,3.13214295375933));
#8421=CARTESIAN_POINT('Ctrl Pts',(2.60425579784155,-1.01431944186932,3.28947826943046));
#8422=CARTESIAN_POINT('Ctrl Pts',(2.27924634057658,1.61741407950708,3.44681358510158));
#8423=CARTESIAN_POINT('Ctrl Pts',(-0.0975982492034651,2.79311059143494,
3.6041489007727));
#8424=CARTESIAN_POINT('Ctrl Pts',(-2.04600507844241,1.65356799864077,3.73807433637385));
#8425=CARTESIAN_POINT('Ctrl Pts',(-2.36710223082098,0.433557734928271,3.81955466675129));
#8426=CARTESIAN_POINT('Ctrl Pts',(-2.36819322153198,-0.000653453332863235,
3.84858989190502));
#8427=CARTESIAN_POINT('Origin',(0.,0.,-1.84858989190501));
#8428=CARTESIAN_POINT('',(-2.36804188512505,-0.000112073902353324,1.65141010809498));
#8429=CARTESIAN_POINT('',(-2.37344137975612,-0.00178937704920473,1.84858989190502));
#8430=CARTESIAN_POINT('',(-2.37175,-1.78696459712734E-13,-1.84858989190501));
#8431=CARTESIAN_POINT('Ctrl Pts',(-2.36804188512505,-0.000112073902353224,
1.65141010809498));
#8432=CARTESIAN_POINT('Ctrl Pts',(-2.36821023678956,-0.384577180330964,
1.67711462161287));
#8433=CARTESIAN_POINT('Ctrl Pts',(-2.09930421630608,-1.55226751145704,1.75519863963526));
#8434=CARTESIAN_POINT('Ctrl Pts',(-0.275973625536248,-2.77999224892802,
1.88566216216216));
#8435=CARTESIAN_POINT('Ctrl Pts',(2.16802781286073,-1.76187209738162,2.04280067567567));
#8436=CARTESIAN_POINT('Ctrl Pts',(2.66479327803676,0.838697048159531,2.19993918918919));
#8437=CARTESIAN_POINT('Ctrl Pts',(0.76814623510466,2.68597898024514,2.3570777027027));
#8438=CARTESIAN_POINT('Ctrl Pts',(-1.70898688612053,2.14473275169325,2.50756800900463));
#8439=CARTESIAN_POINT('Ctrl Pts',(-2.36892240045369,0.678044518839718,2.60567881080206));
#8440=CARTESIAN_POINT('Ctrl Pts',(-2.37406517885066,-0.00153607482357281,
2.65141010809498));
#8441=CARTESIAN_POINT('Ctrl Pts',(-2.37344137975612,-0.00178937704920463,
1.84858989190502));
#8442=CARTESIAN_POINT('Ctrl Pts',(-2.37447812169567,-0.12506848067989,1.85688007073346));
#8443=CARTESIAN_POINT('Ctrl Pts',(-2.31006431944847,-1.02714724785255,1.91761535478561));
#8444=CARTESIAN_POINT('Ctrl Pts',(-1.15481219883121,-2.54507342378116,2.03079574406147));
#8445=CARTESIAN_POINT('Ctrl Pts',(1.49072764255621,-2.36404822464922,2.18813105973259));
#8446=CARTESIAN_POINT('Ctrl Pts',(2.79427705549031,-0.0548463935276453,
2.34546637540372));
#8447=CARTESIAN_POINT('Ctrl Pts',(1.5823475414007,2.30372918060613,2.50280169107483));
#8448=CARTESIAN_POINT('Ctrl Pts',(-1.05405113312049,2.58842974112365,2.66013700674597));
#8449=CARTESIAN_POINT('Ctrl Pts',(-2.29031280961247,1.08993341565411,2.77539974035602));
#8450=CARTESIAN_POINT('Ctrl Pts',(-2.37393373216083,0.15638533864836,2.83821736874238));
#8451=CARTESIAN_POINT('Ctrl Pts',(-2.37255724078598,0.00199178475905658,
2.84858989190502));
#8452=CARTESIAN_POINT('Origin',(0.,0.,-1.84858989190501));
#8453=CARTESIAN_POINT('',(-2.37366757034868,0.00184471646948807,0.651410108094983));
#8454=CARTESIAN_POINT('',(-2.36802324146013,0.000186122305323028,0.848589891905023));
#8455=CARTESIAN_POINT('',(-2.37175,-1.78696459712734E-13,-1.84858989190501));
#8456=CARTESIAN_POINT('Ctrl Pts',(-2.37366757034868,0.001844716469488,0.651410108094984));
#8457=CARTESIAN_POINT('Ctrl Pts',(-2.36827887140227,-0.663567421798888,
0.696170927919177));
#8458=CARTESIAN_POINT('Ctrl Pts',(-1.73206830317985,-2.11713322740477,0.793311252247876));
#8459=CARTESIAN_POINT('Ctrl Pts',(0.718910407331439,-2.69944634094777,0.942831081081078));
#8460=CARTESIAN_POINT('Ctrl Pts',(2.64899289676255,-0.887370898887054,1.09996959459459));
#8461=CARTESIAN_POINT('Ctrl Pts',(2.19990031581894,1.72195501972256,1.25710810810811));
#8462=CARTESIAN_POINT('Ctrl Pts',(-0.225079684819506,2.78455874530281,1.41424662162162));
#8463=CARTESIAN_POINT('Ctrl Pts',(-2.08428517335687,1.58152664346482,1.54568062161725));
#8464=CARTESIAN_POINT('Ctrl Pts',(-2.36786717732013,0.39886856587965,1.62473511710837));
#8465=CARTESIAN_POINT('Ctrl Pts',(-2.36804188512505,-0.000112073902353224,
1.65141010809498));
#8466=CARTESIAN_POINT('Ctrl Pts',(-2.36802324146013,0.000186122305323062,
0.848589891905023));
#8467=CARTESIAN_POINT('Ctrl Pts',(-2.36776001721126,-0.402962357372647,
0.87554277272455));
#8468=CARTESIAN_POINT('Ctrl Pts',(-2.0797505690667,-1.59092671500009,0.954940758767785));
#8469=CARTESIAN_POINT('Ctrl Pts',(-0.207121339063888,-2.78711087979173,
1.08678385003473));
#8470=CARTESIAN_POINT('Ctrl Pts',(2.21401803077907,-1.70561830406782,1.24411916570585));
#8471=CARTESIAN_POINT('Ctrl Pts',(2.64205485235054,0.911349150745493,1.40145448137697));
#8472=CARTESIAN_POINT('Ctrl Pts',(0.691640660298454,2.70787919402874,1.5587897970481));
#8473=CARTESIAN_POINT('Ctrl Pts',(-1.74582592441822,2.10050088985172,1.70783493389078));
#8474=CARTESIAN_POINT('Ctrl Pts',(-2.36791951286044,0.654816452515466,1.80443496550976));
#8475=CARTESIAN_POINT('Ctrl Pts',(-2.37344137975612,-0.00178937704920463,
1.84858989190502));
#8476=CARTESIAN_POINT('Origin',(0.,0.,11.5));
#8477=CARTESIAN_POINT('',(-2.86997293948595,0.000709208322249463,11.1339652973708));
#8478=CARTESIAN_POINT('Ctrl Pts',(-0.439445221994061,2.3306835819919,11.62825));
#8479=CARTESIAN_POINT('Ctrl Pts',(-0.359483020814685,2.34931149018937,11.6247602761445));
#8480=CARTESIAN_POINT('Ctrl Pts',(-0.27871400731898,2.36341693162049,11.6212847858384));
#8481=CARTESIAN_POINT('Ctrl Pts',(-0.197463562604575,2.37318447045242,11.6178187998135));
#8482=CARTESIAN_POINT('Ctrl Pts',(-0.114065564321399,2.38321017787593,11.614261203328));
#8483=CARTESIAN_POINT('Ctrl Pts',(-0.0301595928545948,2.38866567182183,
11.6107136201843));
#8484=CARTESIAN_POINT('Ctrl Pts',(0.0539178478306465,2.38969830818771,11.6071709361129));
#8485=CARTESIAN_POINT('Ctrl Pts',(0.0934462943689916,2.39018379527021,11.6055053668855));
#8486=CARTESIAN_POINT('Ctrl Pts',(0.133012786809523,2.38969093626847,11.6038408805234));
#8487=CARTESIAN_POINT('Ctrl Pts',(0.172582728329755,2.38823118545469,11.6021769455617));
#8488=CARTESIAN_POINT('Ctrl Pts',(0.196983674678661,2.38733102488025,11.6011508741002));
#8489=CARTESIAN_POINT('Ctrl Pts',(0.221385934120707,2.38606314465001,11.6001250123152));
#8490=CARTESIAN_POINT('Ctrl Pts',(0.24578137026875,2.38442977721171,11.5990992355836));
#8491=CARTESIAN_POINT('Ctrl Pts',(0.261730484740349,2.38336192320454,11.5984286088969));
#8492=CARTESIAN_POINT('Ctrl Pts',(0.277677591321838,2.38213767553654,11.597757980196));
#8493=CARTESIAN_POINT('Ctrl Pts',(0.293603734342933,2.38075929535175,11.5970880163414));
#8494=CARTESIAN_POINT('Ctrl Pts',(0.379341030417818,2.37333888038685,11.5934813119885));
#8495=CARTESIAN_POINT('Ctrl Pts',(0.464583014225527,2.36144918428767,11.5898891320915));
#8496=CARTESIAN_POINT('Ctrl Pts',(0.548977057540434,2.34525221307984,11.5863062427765));
#8497=CARTESIAN_POINT('Ctrl Pts',(0.63410785152571,2.32891384410355,11.5826920752337));
#8498=CARTESIAN_POINT('Ctrl Pts',(0.718376786391574,2.30819252148602,11.5790873611926));
#8499=CARTESIAN_POINT('Ctrl Pts',(0.801421129360431,2.28320149524268,11.5754867285058));
#8500=CARTESIAN_POINT('Ctrl Pts',(0.851520069054253,2.26812492443856,11.5733145410529));
#8501=CARTESIAN_POINT('Ctrl Pts',(0.901173245121242,2.25149340059607,11.5711438389925));
#8502=CARTESIAN_POINT('Ctrl Pts',(0.950298631716725,2.23332291784394,11.5689734428101));
#8503=CARTESIAN_POINT('Ctrl Pts',(0.963508179039198,2.22843697457875,11.5683898351671));
#8504=CARTESIAN_POINT('Ctrl Pts',(0.976678902975083,2.22343988211883,11.5678062771152));
#8505=CARTESIAN_POINT('Ctrl Pts',(0.989796896482515,2.2183369213822,11.5672232951128));
#8506=CARTESIAN_POINT('Ctrl Pts',(1.0715488401239,2.18653503351653,11.5635901242489));
#8507=CARTESIAN_POINT('Ctrl Pts',(1.15137916677557,2.15057972741051,11.5599737688071));
#8508=CARTESIAN_POINT('Ctrl Pts',(1.22892868995964,2.11061806082819,11.5563689172299));
#8509=CARTESIAN_POINT('Ctrl Pts',(1.30609743699769,2.07085261014462,11.5527817658451));
#8510=CARTESIAN_POINT('Ctrl Pts',(1.38100867140758,2.02711976610499,11.5492060056319));
#8511=CARTESIAN_POINT('Ctrl Pts',(1.45329568150197,1.97951483102432,11.5456364028898));
#8512=CARTESIAN_POINT('Ctrl Pts',(1.51120974849783,1.94137526215855,11.5427765500327));
#8513=CARTESIAN_POINT('Ctrl Pts',(1.56743935204678,1.90074932215926,11.5399206494764));
#8514=CARTESIAN_POINT('Ctrl Pts',(1.621783737959,1.85766460010194,11.5370660098083));
#8515=CARTESIAN_POINT('Ctrl Pts',(1.64895593091511,1.83612223907328,11.5356386899743));
#8516=CARTESIAN_POINT('Ctrl Pts',(1.67565661487015,1.81396489287275,11.5342116853624));
#8517=CARTESIAN_POINT('Ctrl Pts',(1.70185926132131,1.79119431574093,11.532784659546));
#8518=CARTESIAN_POINT('Ctrl Pts',(1.71882166156475,1.77645368090452,11.5318608680083));
#8519=CARTESIAN_POINT('Ctrl Pts',(1.73557532962421,1.76145603809249,11.5309370675846));
#8520=CARTESIAN_POINT('Ctrl Pts',(1.75211281381839,1.74620161928424,11.5300131670071));
#8521=CARTESIAN_POINT('Ctrl Pts',(1.76112158754248,1.73789179381609,11.529509873329));
#8522=CARTESIAN_POINT('Ctrl Pts',(1.77006808708219,1.72950393138366,11.5290064421071));
#8523=CARTESIAN_POINT('Ctrl Pts',(1.77894146971999,1.72104732904951,11.5285034067769));
#8524=CARTESIAN_POINT('Ctrl Pts',(1.83933200754334,1.66349331791721,11.5250798449438));
#8525=CARTESIAN_POINT('Ctrl Pts',(1.8963984276916,1.60270624192685,11.5216713230637));
#8526=CARTESIAN_POINT('Ctrl Pts',(1.95011819953022,1.53907807970147,11.5182734051049));
#8527=CARTESIAN_POINT('Ctrl Pts',(2.00542449571231,1.47357076525995,11.5147751352761));
#8528=CARTESIAN_POINT('Ctrl Pts',(2.05718398574646,1.40505149787053,11.511288104956));
#8529=CARTESIAN_POINT('Ctrl Pts',(2.10533946111886,1.3339039115796,11.5078074733588));
#8530=CARTESIAN_POINT('Ctrl Pts',(2.15154257592138,1.26564085173229,11.5044679565119));
#8531=CARTESIAN_POINT('Ctrl Pts',(2.19442802485129,1.19495736996561,11.5011343300606));
#8532=CARTESIAN_POINT('Ctrl Pts',(2.23391281993103,1.12216394079048,11.4978023184486));
#8533=CARTESIAN_POINT('Ctrl Pts',(2.25118741777841,1.09031681552637,11.4963445633684));
#8534=CARTESIAN_POINT('Ctrl Pts',(2.26781067606573,1.05806553560368,11.4948871173785));
#8535=CARTESIAN_POINT('Ctrl Pts',(2.28377353610697,1.02543493097626,11.4934296224428));
#8536=CARTESIAN_POINT('Ctrl Pts',(2.29326703470383,1.00602872191068,11.4925628149854));
#8537=CARTESIAN_POINT('Ctrl Pts',(2.30252692730832,0.986488335264957,11.4916959902159));
#8538=CARTESIAN_POINT('Ctrl Pts',(2.31155107931692,0.966818908506685,11.4908290728209));
#8539=CARTESIAN_POINT('Ctrl Pts',(2.31863529945096,0.951377840034761,11.490148517611));
#8540=CARTESIAN_POINT('Ctrl Pts',(2.32557538886546,0.935854346809815,11.4894677807698));
#8541=CARTESIAN_POINT('Ctrl Pts',(2.33236053374086,0.920273937348818,11.4887878255595));
#8542=CARTESIAN_POINT('Ctrl Pts',(2.36796902716184,0.838507826532316,11.4852194152932));
#8543=CARTESIAN_POINT('Ctrl Pts',(2.39937221583678,0.755052917299449,11.4816670269197));
#8544=CARTESIAN_POINT('Ctrl Pts',(2.42650990964853,0.670313949715511,11.4781256336386));
#8545=CARTESIAN_POINT('Ctrl Pts',(2.45395171326163,0.584625382258507,11.4745445548773));
#8546=CARTESIAN_POINT('Ctrl Pts',(2.47703230477293,0.497622920338958,11.470974719015));
#8547=CARTESIAN_POINT('Ctrl Pts',(2.49564463758615,0.409696684762178,11.4674109283565));
#8548=CARTESIAN_POINT('Ctrl Pts',(2.51256694354607,0.329754279086013,11.464170735066));
#8549=CARTESIAN_POINT('Ctrl Pts',(2.52579526118549,0.24904737731457,11.460935538995));
#8550=CARTESIAN_POINT('Ctrl Pts',(2.53521313973642,0.167858755145902,11.4577014336506));
#8551=CARTESIAN_POINT('Ctrl Pts',(2.53942638325848,0.131537684050459,11.4562546032081));
#8552=CARTESIAN_POINT('Ctrl Pts',(2.54287653840534,0.0951201284473648,11.4548079910601));
#8553=CARTESIAN_POINT('Ctrl Pts',(2.54555076253572,0.0586312673898904,11.4533612474409));
#8554=CARTESIAN_POINT('Ctrl Pts',(2.54678080763582,0.0418477284777441,11.4526957983935));
#8555=CARTESIAN_POINT('Ctrl Pts',(2.54784667039524,0.0250491043820508,11.4520303215313));
#8556=CARTESIAN_POINT('Ctrl Pts',(2.54874698931854,0.00823785327091157,
11.4513647828174));
#8557=CARTESIAN_POINT('Ctrl Pts',(2.54950258918657,-0.00587112388394168,
11.4508062241208));
#8558=CARTESIAN_POINT('Ctrl Pts',(2.55014158604825,-0.0199907301096276,
11.4502475533557));
#8559=CARTESIAN_POINT('Ctrl Pts',(2.55066270854233,-0.0341027028361791,
11.4496894146469));
#8560=CARTESIAN_POINT('Ctrl Pts',(2.55400035119776,-0.124485909584641,11.4461146935723));
#8561=CARTESIAN_POINT('Ctrl Pts',(2.55251590030915,-0.214700787372498,11.4425560101414));
#8562=CARTESIAN_POINT('Ctrl Pts',(2.54610973516166,-0.304360270645855,11.4390083150826));
#8563=CARTESIAN_POINT('Ctrl Pts',(2.53992350143221,-0.390941635131681,11.4355824166973));
#8564=CARTESIAN_POINT('Ctrl Pts',(2.52914771427487,-0.477005973362024,11.4321667651471));
#8565=CARTESIAN_POINT('Ctrl Pts',(2.51364702202946,-0.56221151242787,11.4287568135539));
#8566=CARTESIAN_POINT('Ctrl Pts',(2.4978416408886,-0.649091891634602,11.4252798343488));
#8567=CARTESIAN_POINT('Ctrl Pts',(2.47712400969773,-0.735080204165537,11.4218087813851));
#8568=CARTESIAN_POINT('Ctrl Pts',(2.45176245019841,-0.819915179815436,11.4183388343531));
#8569=CARTESIAN_POINT('Ctrl Pts',(2.43759878319083,-0.867292958210081,11.4164009734618));
#8570=CARTESIAN_POINT('Ctrl Pts',(2.42198578511571,-0.914310849766526,11.4144634574981));
#8571=CARTESIAN_POINT('Ctrl Pts',(2.40496360252248,-0.960921226687823,11.4125254468584));
#8572=CARTESIAN_POINT('Ctrl Pts',(2.39839032938233,-0.978920254544038,11.4117770661373));
#8573=CARTESIAN_POINT('Ctrl Pts',(2.39160484182306,-0.996863365779891,11.4110284061025));
#8574=CARTESIAN_POINT('Ctrl Pts',(2.38462104532031,-1.01471861919519,11.4102806421704));
#8575=CARTESIAN_POINT('Ctrl Pts',(2.35196925304181,-1.09819843212604,11.4067845734384));
#8576=CARTESIAN_POINT('Ctrl Pts',(2.31495075727319,-1.17986515814379,11.4033036769767));
#8577=CARTESIAN_POINT('Ctrl Pts',(2.27389075093231,-1.25946542646749,11.3998332297369));
#8578=CARTESIAN_POINT('Ctrl Pts',(2.23207387867294,-1.34053297976178,11.3962988111666));
#8579=CARTESIAN_POINT('Ctrl Pts',(2.18606471254661,-1.41945796930655,11.3927752305933));
#8580=CARTESIAN_POINT('Ctrl Pts',(2.13615274225743,-1.49596025824322,11.3892574989426));
#8581=CARTESIAN_POINT('Ctrl Pts',(2.08602408315185,-1.57279467573233,11.385724495342));
#8582=CARTESIAN_POINT('Ctrl Pts',(2.03195810671375,-1.64718611516111,11.3821973915595));
#8583=CARTESIAN_POINT('Ctrl Pts',(1.97420160691916,-1.71882633760539,11.3786711332592));
#8584=CARTESIAN_POINT('Ctrl Pts',(1.95240508667088,-1.74586238661548,11.377340371168));
#8585=CARTESIAN_POINT('Ctrl Pts',(1.93008253152955,-1.77250629512415,11.3760097294909));
#8586=CARTESIAN_POINT('Ctrl Pts',(1.90724574604483,-1.79874022848494,11.3746789365696));
#8587=CARTESIAN_POINT('Ctrl Pts',(1.89585779635524,-1.81182222347379,11.3740153141501));
#8588=CARTESIAN_POINT('Ctrl Pts',(1.8843419621495,-1.82480225835256,11.3733516541209));
#8589=CARTESIAN_POINT('Ctrl Pts',(1.87269964124851,-1.83767804526001,11.3726879227956));
#8590=CARTESIAN_POINT('Ctrl Pts',(1.86326625859819,-1.8481108640987,11.3721501235353));
#8591=CARTESIAN_POINT('Ctrl Pts',(1.8537496389451,-1.8584753407347,11.3716122696922));
#8592=CARTESIAN_POINT('Ctrl Pts',(1.8441608279676,-1.86875948192732,11.3710749125616));
#8593=CARTESIAN_POINT('Ctrl Pts',(1.78056218360928,-1.93696996597738,11.3675108434478));
#8594=CARTESIAN_POINT('Ctrl Pts',(1.71368420494736,-2.00176842633816,11.3639624618779));
#8595=CARTESIAN_POINT('Ctrl Pts',(1.64382533951827,-2.06287172496906,11.3604247664903));
#8596=CARTESIAN_POINT('Ctrl Pts',(1.57423141411002,-2.12374328910052,11.3569004878264));
#8597=CARTESIAN_POINT('Ctrl Pts',(1.50167852811227,-2.18094842953722,11.3533868144436));
#8598=CARTESIAN_POINT('Ctrl Pts',(1.42641996197867,-2.2341772386581,11.3498788016679));
#8599=CARTESIAN_POINT('Ctrl Pts',(1.3516762241841,-2.28704192046701,11.3463947864845));
#8600=CARTESIAN_POINT('Ctrl Pts',(1.27426307539374,-2.33598522008376,11.342916354727));
#8601=CARTESIAN_POINT('Ctrl Pts',(1.19439676647842,-2.38066281826916,11.339438662505));
#8602=CARTESIAN_POINT('Ctrl Pts',(1.15339338620205,-2.40360030684365,11.3376532145659));
#8603=CARTESIAN_POINT('Ctrl Pts',(1.11174294293827,-2.42541271468527,11.3358679615534));
#8604=CARTESIAN_POINT('Ctrl Pts',(1.06947220915485,-2.44604826098259,11.334082247983));
#8605=CARTESIAN_POINT('Ctrl Pts',(1.05124776879456,-2.45494499044852,11.3333123623541));
#8606=CARTESIAN_POINT('Ctrl Pts',(1.0329023157667,-2.46362538871231,11.3325421557385));
#8607=CARTESIAN_POINT('Ctrl Pts',(1.01446903163988,-2.47207123914098,11.3317728670993));
#8608=CARTESIAN_POINT('Ctrl Pts',(0.992379075227472,-2.48219252119531,11.3308509720972));
#8609=CARTESIAN_POINT('Ctrl Pts',(0.970156538466361,-2.49198036655811,11.3299301186847));
#8610=CARTESIAN_POINT('Ctrl Pts',(0.94780620569595,-2.50142961190602,11.3290102203308));
#8611=CARTESIAN_POINT('Ctrl Pts',(0.865790439448149,-2.53610413356231,11.3256346031023));
#8612=CARTESIAN_POINT('Ctrl Pts',(0.78205610317221,-2.56622272676918,11.3222718463403));
#8613=CARTESIAN_POINT('Ctrl Pts',(0.696974578785958,-2.59191739767486,11.318917674299));
#8614=CARTESIAN_POINT('Ctrl Pts',(0.609579162327931,-2.61831086536073,11.3154722816062));
#8615=CARTESIAN_POINT('Ctrl Pts',(0.520761565645775,-2.64003666842693,11.3120359469267));
#8616=CARTESIAN_POINT('Ctrl Pts',(0.430899300361841,-2.65718927641842,11.3086040360895));
#8617=CARTESIAN_POINT('Ctrl Pts',(0.343209845834361,-2.67392714557567,11.3052551066101));
#8618=CARTESIAN_POINT('Ctrl Pts',(0.25452479015491,-2.6863100783274,11.3019103896282));
#8619=CARTESIAN_POINT('Ctrl Pts',(0.165183352753207,-2.69438132192965,11.2985655790638));
#8620=CARTESIAN_POINT('Ctrl Pts',(0.137834848150192,-2.69685202812409,11.2975416917191));
#8621=CARTESIAN_POINT('Ctrl Pts',(0.110424801620538,-2.69891839950379,11.2965177956053));
#8622=CARTESIAN_POINT('Ctrl Pts',(0.08296290180991,-2.70058085938097,11.2954937672061));
#8623=CARTESIAN_POINT('Ctrl Pts',(0.0669684788561147,-2.70154911309258,
11.2948973502268));
#8624=CARTESIAN_POINT('Ctrl Pts',(0.0509564666454086,-2.70238034652659,
11.2943008883741));
#8625=CARTESIAN_POINT('Ctrl Pts',(0.0349287839010169,-2.70307458363613,
11.2937043572455));
#8626=CARTESIAN_POINT('Ctrl Pts',(0.0206834334719444,-2.70369161924033,
11.293174162388));
#8627=CARTESIAN_POINT('Ctrl Pts',(0.00643409067270473,-2.70420004997344,
11.2926442249703));
#8628=CARTESIAN_POINT('Ctrl Pts',(-0.00781400179505987,-2.70460019597085,
11.2921146711228));
#8629=CARTESIAN_POINT('Ctrl Pts',(-0.101952151334104,-2.70724398873305,
11.2886158715889));
#8630=CARTESIAN_POINT('Ctrl Pts',(-0.196088226677417,-2.7051673117304,11.2851318105594));
#8631=CARTESIAN_POINT('Ctrl Pts',(-0.289825667638303,-2.6984813516168,11.2816577549713));
#8632=CARTESIAN_POINT('Ctrl Pts',(-0.384631538117472,-2.69171918420471,
11.2781441017209));
#8633=CARTESIAN_POINT('Ctrl Pts',(-0.479030586990251,-2.68024208441543,
11.2746406832979));
#8634=CARTESIAN_POINT('Ctrl Pts',(-0.57262152425153,-2.66411259564997,11.2711426029439));
#8635=CARTESIAN_POINT('Ctrl Pts',(-0.666559717691804,-2.64792326065578,
11.2676315434484));
#8636=CARTESIAN_POINT('Ctrl Pts',(-0.759684799865766,-2.62704692522732,
11.2641258617076));
#8637=CARTESIAN_POINT('Ctrl Pts',(-0.851585181919148,-2.6014943492988,11.2606206062542));
#8638=CARTESIAN_POINT('Ctrl Pts',(-0.886047825189167,-2.59191213332561,
11.2593061354592));
#8639=CARTESIAN_POINT('Ctrl Pts',(-0.920338108563248,-2.58167179563189,
11.2579917246108));
#8640=CARTESIAN_POINT('Ctrl Pts',(-0.95443366677234,-2.57077201863537,11.2566771125966));
#8641=CARTESIAN_POINT('Ctrl Pts',(-0.974280480974564,-2.5644273256531,11.255911885049));
#8642=CARTESIAN_POINT('Ctrl Pts',(-0.99406130744013,-2.55785917358927,11.2551465893396));
#8643=CARTESIAN_POINT('Ctrl Pts',(-1.01377165408274,-2.55106714297751,11.2543811739687));
#8644=CARTESIAN_POINT('Ctrl Pts',(-1.02736841414217,-2.54638180627496,11.2538531685848));
#8645=CARTESIAN_POINT('Ctrl Pts',(-1.04092225787931,-2.54159315279905,11.253325470206));
#8646=CARTESIAN_POINT('Ctrl Pts',(-1.05443025528497,-2.53670205395909,11.252798124302));
#8647=CARTESIAN_POINT('Ctrl Pts',(-1.14463510839177,-2.50403985843604,11.2492765690056));
#8648=CARTESIAN_POINT('Ctrl Pts',(-1.23281912858369,-2.46680540724472,11.2457698275395));
#8649=CARTESIAN_POINT('Ctrl Pts',(-1.31858159439492,-2.42506535814129,11.242273074989));
#8650=CARTESIAN_POINT('Ctrl Pts',(-1.40311199337542,-2.38392494816353,11.2388265569179));
#8651=CARTESIAN_POINT('Ctrl Pts',(-1.48529083212456,-2.33840727081253,11.2353897428216));
#8652=CARTESIAN_POINT('Ctrl Pts',(-1.56472199239298,-2.28852750879454,11.2319580127567));
#8653=CARTESIAN_POINT('Ctrl Pts',(-1.58551758994019,-2.27546866069046,11.2310595633688));
#8654=CARTESIAN_POINT('Ctrl Pts',(-1.60612474663732,-2.26211056997792,11.230161462454));
#8655=CARTESIAN_POINT('Ctrl Pts',(-1.62653609083598,-2.2484529714829,11.2292636271078));
#8656=CARTESIAN_POINT('Ctrl Pts',(-1.70441968299709,-2.19633965543995,11.225837755629));
#8657=CARTESIAN_POINT('Ctrl Pts',(-1.77945485532057,-2.13986885585993,11.222415750716));
#8658=CARTESIAN_POINT('Ctrl Pts',(-1.85149349468849,-2.07939019092048,11.2189930066095));
#8659=CARTESIAN_POINT('Ctrl Pts',(-1.8748645479439,-2.05976946915896,11.2178825867641));
#8660=CARTESIAN_POINT('Ctrl Pts',(-1.89791995295043,-2.03972659946025,11.2167720891179));
#8661=CARTESIAN_POINT('Ctrl Pts',(-1.92065386067013,-2.01927267290743,11.2156613564032));
#8662=CARTESIAN_POINT('Ctrl Pts',(-1.9316413592642,-2.00938710936888,11.2151245294621));
#8663=CARTESIAN_POINT('Ctrl Pts',(-1.94255421950186,-1.99940498570623,11.2145876221361));
#8664=CARTESIAN_POINT('Ctrl Pts',(-1.95338011991677,-1.98933864610605,11.2140511999421));
#8665=CARTESIAN_POINT('Ctrl Pts',(-2.02242773931489,-1.92513550744723,11.2106298978731));
#8666=CARTESIAN_POINT('Ctrl Pts',(-2.08805585991204,-1.85740773886018,11.2072227031525));
#8667=CARTESIAN_POINT('Ctrl Pts',(-2.15015903930769,-1.7865606665237,11.2038251982962));
#8668=CARTESIAN_POINT('Ctrl Pts',(-2.21349481278046,-1.71430745552261,11.2003602613952));
#8669=CARTESIAN_POINT('Ctrl Pts',(-2.27316487566809,-1.63880924004706,11.1969054028151));
#8670=CARTESIAN_POINT('Ctrl Pts',(-2.32902567586957,-1.56045035084564,11.1934559367882));
#8671=CARTESIAN_POINT('Ctrl Pts',(-2.38527990190259,-1.48153958249049,11.1899821762823));
#8672=CARTESIAN_POINT('Ctrl Pts',(-2.43767154642151,-1.39972691196139,11.1865138845562));
#8673=CARTESIAN_POINT('Ctrl Pts',(-2.48601414345046,-1.31537014370798,11.1830462761383));
#8674=CARTESIAN_POINT('Ctrl Pts',(-2.51324863986033,-1.26784654664574,11.1810927491288));
#8675=CARTESIAN_POINT('Ctrl Pts',(-2.53919729042327,-1.21951494628862,11.1791394389872));
#8676=CARTESIAN_POINT('Ctrl Pts',(-2.56382026308967,-1.17043597842562,11.1771854900701));
#8677=CARTESIAN_POINT('Ctrl Pts',(-2.57043915220293,-1.15724308533024,11.1766602500274));
#8678=CARTESIAN_POINT('Ctrl Pts',(-2.57696321367054,-1.1439941193146,11.1761348825453));
#8679=CARTESIAN_POINT('Ctrl Pts',(-2.58338840616944,-1.13069688731366,11.175609633533));
#8680=CARTESIAN_POINT('Ctrl Pts',(-2.62620034331217,-1.04209561027884,11.172109827464));
#8681=CARTESIAN_POINT('Ctrl Pts',(-2.66450788394824,-0.951602474453648,
11.1686250464566));
#8682=CARTESIAN_POINT('Ctrl Pts',(-2.69817002472794,-0.859613847080416,
11.1651505728457));
#8683=CARTESIAN_POINT('Ctrl Pts',(-2.73183382450822,-0.767620686151626,
11.1616759279993));
#8684=CARTESIAN_POINT('Ctrl Pts',(-2.76085223666098,-0.67413102162785,11.1582115915653));
#8685=CARTESIAN_POINT('Ctrl Pts',(-2.78504109696179,-0.579512179774996,
11.1547528451809));
#8686=CARTESIAN_POINT('Ctrl Pts',(-2.80867562760501,-0.487061692675289,
11.1513733619645));
#8687=CARTESIAN_POINT('Ctrl Pts',(-2.8276996967141,-0.393532337548253,11.1479992155222));
#8688=CARTESIAN_POINT('Ctrl Pts',(-2.84189514122644,-0.299251761426908,
11.1446260045022));
#8689=CARTESIAN_POINT('Ctrl Pts',(-2.85324010443846,-0.223902964369238,
11.1419301428196));
#8690=CARTESIAN_POINT('Ctrl Pts',(-2.86150015598816,-0.148073915036915,
11.1392348786069));
#8691=CARTESIAN_POINT('Ctrl Pts',(-2.86653995619031,-0.0719300717664526,
11.1365379651471));
#8692=CARTESIAN_POINT('Ctrl Pts',(-2.86814414143213,-0.0476932320643782,
11.1356795285827));
#8693=CARTESIAN_POINT('Ctrl Pts',(-2.86941988081495,-0.0234547494955555,
11.1348219958471));
#8694=CARTESIAN_POINT('Ctrl Pts',(-2.87036479087719,0.000779773978368722,
11.1339652973708));
#8695=CARTESIAN_POINT('',(0.261199069988913,2.92594434598213,11.058));
#8696=CARTESIAN_POINT('Ctrl Pts',(0.261124777554784,2.92529416030266,11.058));
#8697=CARTESIAN_POINT('Ctrl Pts',(0.163252076286772,2.9214051496811,11.0703793245688));
#8698=CARTESIAN_POINT('Ctrl Pts',(0.0658388360676064,2.91286361031638,11.0828028087884));
#8699=CARTESIAN_POINT('Ctrl Pts',(-0.0307369711720644,2.89968653111402,
11.0952900032599));
#8700=CARTESIAN_POINT('Ctrl Pts',(-0.12623809978967,2.88665608413482,11.1076382424244));
#8701=CARTESIAN_POINT('Ctrl Pts',(-0.220921197195477,2.86909236615812,11.1200487818169));
#8702=CARTESIAN_POINT('Ctrl Pts',(-0.31439997383375,2.84696555496448,11.1325405266072));
#8703=CARTESIAN_POINT('Ctrl Pts',(-0.389995520831668,2.82907177783499,11.1426425017756));
#8704=CARTESIAN_POINT('Ctrl Pts',(-0.464803253647579,2.80819289824412,11.152797583885));
#8705=CARTESIAN_POINT('Ctrl Pts',(-0.538603048202427,2.78429272567688,11.1630157713274));
#8706=CARTESIAN_POINT('Ctrl Pts',(-0.593952894118562,2.76636759625145,11.1706794119091));
#8707=CARTESIAN_POINT('Ctrl Pts',(-0.648735503576454,2.7467426089957,11.1783785492407));
#8708=CARTESIAN_POINT('Ctrl Pts',(-0.702851172581185,2.72539620337798,11.1861174013937));
#8709=CARTESIAN_POINT('Ctrl Pts',(-0.71873840261759,2.71912934457837,11.1883893667345));
#8710=CARTESIAN_POINT('Ctrl Pts',(-0.734568107078247,2.71271408483162,11.190664755044));
#8711=CARTESIAN_POINT('Ctrl Pts',(-0.750337652372167,2.70614979460715,11.1929436730527));
#8712=CARTESIAN_POINT('Ctrl Pts',(-0.763539656096334,2.70065427889159,11.1948515456945));
#8713=CARTESIAN_POINT('Ctrl Pts',(-0.776691326847496,2.69505769580723,11.1967607130315));
#8714=CARTESIAN_POINT('Ctrl Pts',(-0.789788993683481,2.68936106997679,11.1986708957826));
#8715=CARTESIAN_POINT('Ctrl Pts',(-0.87317349082548,2.65309428397392,11.2108318119326));
#8716=CARTESIAN_POINT('Ctrl Pts',(-0.954403883416443,2.61276259333994,11.2230385405707));
#8717=CARTESIAN_POINT('Ctrl Pts',(-1.03314628688233,2.56834468618871,11.2353100289649));
#8718=CARTESIAN_POINT('Ctrl Pts',(-1.07823214235908,2.54291214597843,11.2423363645588));
#8719=CARTESIAN_POINT('Ctrl Pts',(-1.12250179725942,2.51613922516579,11.2493839310575));
#8720=CARTESIAN_POINT('Ctrl Pts',(-1.16588734321926,2.48801620495338,11.2564562851141));
#8721=CARTESIAN_POINT('Ctrl Pts',(-1.2435976078222,2.43764349916415,11.2691239718505));
#8722=CARTESIAN_POINT('Ctrl Pts',(-1.31847408700313,2.38294042952196,11.2818711829841));
#8723=CARTESIAN_POINT('Ctrl Pts',(-1.39030087935118,2.32423346489716,11.2947183566611));
#8724=CARTESIAN_POINT('Ctrl Pts',(-1.46342993694969,2.26446210581046,11.3077984577361));
#8725=CARTESIAN_POINT('Ctrl Pts',(-1.53339828473794,2.20053932645019,11.3209821789827));
#8726=CARTESIAN_POINT('Ctrl Pts',(-1.59992558939365,2.1327921427514,11.3342910904939));
#8727=CARTESIAN_POINT('Ctrl Pts',(-1.61340208445737,2.11906853570881,11.3369870884937));
#8728=CARTESIAN_POINT('Ctrl Pts',(-1.62674073455187,2.10518403555254,11.3396889690338));
#8729=CARTESIAN_POINT('Ctrl Pts',(-1.63991787601809,2.09116421105248,11.3423925384684));
#8730=CARTESIAN_POINT('Ctrl Pts',(-1.70139884650346,2.02575150993609,11.3550066606613));
#8731=CARTESIAN_POINT('Ctrl Pts',(-1.75944768512028,1.95731714657644,11.3676731670409));
#8732=CARTESIAN_POINT('Ctrl Pts',(-1.8138993651727,1.88618389956551,11.3804137020214));
#8733=CARTESIAN_POINT('Ctrl Pts',(-1.86815753562372,1.81530344486993,11.393108959871));
#8734=CARTESIAN_POINT('Ctrl Pts',(-1.91884436205444,1.74174225535381,11.4058777210929));
#8735=CARTESIAN_POINT('Ctrl Pts',(-1.96574838356875,1.66580180077525,11.4187414001618));
#8736=CARTESIAN_POINT('Ctrl Pts',(-2.01186212788083,1.59114085290088,11.4313883414761));
#8737=CARTESIAN_POINT('Ctrl Pts',(-2.05431959945996,1.51417923664983,11.4441270290762));
#8738=CARTESIAN_POINT('Ctrl Pts',(-2.09287020326133,1.43520021222363,11.4569778131465));
#8739=CARTESIAN_POINT('Ctrl Pts',(-2.11361694660402,1.39269614256837,11.4638937079073));
#8740=CARTESIAN_POINT('Ctrl Pts',(-2.13323129045024,1.34960780406157,11.4708420687169));
#8741=CARTESIAN_POINT('Ctrl Pts',(-2.15166787184208,1.30598030868302,11.4778260675126));
#8742=CARTESIAN_POINT('Ctrl Pts',(-2.15713184571921,1.29305060712901,11.4798958865407));
#8743=CARTESIAN_POINT('Ctrl Pts',(-2.16249308944786,1.28007170317631,11.4819691313049));
#8744=CARTESIAN_POINT('Ctrl Pts',(-2.16774797314523,1.26705068510794,11.4840449452013));
#8745=CARTESIAN_POINT('Ctrl Pts',(-2.19963752356477,1.18803192158837,11.4966421358759));
#8746=CARTESIAN_POINT('Ctrl Pts',(-2.22751419897903,1.10771397257159,11.5092939385505));
#8747=CARTESIAN_POINT('Ctrl Pts',(-2.25120331746379,1.02636717479289,11.5220225137828));
#8748=CARTESIAN_POINT('Ctrl Pts',(-2.27454503464211,0.946213329121761,11.5345644242532));
#8749=CARTESIAN_POINT('Ctrl Pts',(-2.29382118362004,0.865059764231561,11.5471808720505));
#8750=CARTESIAN_POINT('Ctrl Pts',(-2.30881496364231,0.783166675687281,11.5598930570057));
#8751=CARTESIAN_POINT('Ctrl Pts',(-2.3233692591387,0.703673965509062,11.572232633548));
#8752=CARTESIAN_POINT('Ctrl Pts',(-2.33388845327117,0.623483808186223,11.5846624171728));
#8753=CARTESIAN_POINT('Ctrl Pts',(-2.34012749274977,0.542846284442329,11.5972017976454));
#8754=CARTESIAN_POINT('Ctrl Pts',(-2.34523853245788,0.476787785015864,11.6074740954455));
#8755=CARTESIAN_POINT('Ctrl Pts',(-2.34747636127652,0.410429125649976,11.6178199429796));
#8756=CARTESIAN_POINT('Ctrl Pts',(-2.34668236863853,0.343918483395475,11.62825));
#8757=CARTESIAN_POINT('',(-2.14415473270599,2.01243073062329,11.058));
#8758=CARTESIAN_POINT('Origin',(0.,0.,11.058));
#8759=CARTESIAN_POINT('Ctrl Pts',(-2.87036479087719,0.000779773978368722,
11.1339652973708));
#8760=CARTESIAN_POINT('Ctrl Pts',(-2.87200285191233,0.0427918449624727,
11.1324801566689));
#8761=CARTESIAN_POINT('Ctrl Pts',(-2.87264678506693,0.0847919926152422,
11.1309975229776));
#8762=CARTESIAN_POINT('Ctrl Pts',(-2.87228289058568,0.126751532711213,11.1295170338848));
#8763=CARTESIAN_POINT('Ctrl Pts',(-2.87145802595519,0.221864106052536,11.1261611075067));
#8764=CARTESIAN_POINT('Ctrl Pts',(-2.86545855469524,0.316767622116373,11.1228162005919));
#8765=CARTESIAN_POINT('Ctrl Pts',(-2.85455763680452,0.411156736693552,11.1194780920563));
#8766=CARTESIAN_POINT('Ctrl Pts',(-2.84342076253498,0.507588955704657,11.1160677283208));
#8767=CARTESIAN_POINT('Ctrl Pts',(-2.82716775830471,0.603485022278454,11.1126644604589));
#8768=CARTESIAN_POINT('Ctrl Pts',(-2.80603441756026,0.698520670355508,11.1092637873076));
#8769=CARTESIAN_POINT('Ctrl Pts',(-2.79266006313991,0.75866451866233,11.1071116520374));
#8770=CARTESIAN_POINT('Ctrl Pts',(-2.77733000149192,0.818463754777881,11.1049605559651));
#8771=CARTESIAN_POINT('Ctrl Pts',(-2.76009348614301,0.877834296726592,11.1028093582138));
#8772=CARTESIAN_POINT('Ctrl Pts',(-2.74919109087412,0.915387195473845,11.1014486882808));
#8773=CARTESIAN_POINT('Ctrl Pts',(-2.73752580613221,0.952768545576029,11.1000879776682));
#8774=CARTESIAN_POINT('Ctrl Pts',(-2.72510854264357,0.989956497598032,11.0987269376699));
#8775=CARTESIAN_POINT('Ctrl Pts',(-2.72027063675402,1.00444534308902,11.0981966611375));
#8776=CARTESIAN_POINT('Ctrl Pts',(-2.71531799003855,1.0189064745382,11.0976662739811));
#8777=CARTESIAN_POINT('Ctrl Pts',(-2.71025302608607,1.03333338889234,11.0971359498549));
#8778=CARTESIAN_POINT('Ctrl Pts',(-2.67741979989202,1.12685471435798,11.0936981658637));
#8779=CARTESIAN_POINT('Ctrl Pts',(-2.63998428261572,1.2186200392303,11.0902747408666));
#8780=CARTESIAN_POINT('Ctrl Pts',(-2.59822193704792,1.30830487286322,11.0868612068006));
#8781=CARTESIAN_POINT('Ctrl Pts',(-2.55598691495593,1.39900478155616,11.0834090375144));
#8782=CARTESIAN_POINT('Ctrl Pts',(-2.50932621498891,1.48757769234242,11.0799669843223));
#8783=CARTESIAN_POINT('Ctrl Pts',(-2.45847158858181,1.57367848927911,11.0765304257261));
#8784=CARTESIAN_POINT('Ctrl Pts',(-2.40788866695146,1.65931926911486,11.0731122278858));
#8785=CARTESIAN_POINT('Ctrl Pts',(-2.35315604081231,1.74251510638125,11.0696994660854));
#8786=CARTESIAN_POINT('Ctrl Pts',(-2.29445585803367,1.82290449738493,11.0662875925062));
#8787=CARTESIAN_POINT('Ctrl Pts',(-2.24693123162509,1.88798906090443,11.0635252839489));
#8788=CARTESIAN_POINT('Ctrl Pts',(-2.19680500482205,1.95123384018432,11.0607635576017));
#8789=CARTESIAN_POINT('Ctrl Pts',(-2.14415473270599,2.01243073062329,11.058));
#8790=CARTESIAN_POINT('',(-2.,-2.4492935982947E-16,12.));
#8791=CARTESIAN_POINT('',(-2.5,-3.06161699786838E-16,11.5));
#8792=CARTESIAN_POINT('Origin',(0.,0.,12.));
#8793=CARTESIAN_POINT('Ctrl Pts',(1.70810875200395,-2.39535560853238,-0.329233991005387));
#8794=CARTESIAN_POINT('Ctrl Pts',(2.49644455514999,-1.833199709811,-0.276854486500882));
#8795=CARTESIAN_POINT('Ctrl Pts',(3.46233357982621,0.120022568706166,-0.172095477491873));
#8796=CARTESIAN_POINT('Ctrl Pts',(1.80423238277522,2.96114098648209,-0.0149569639783592));
#8797=CARTESIAN_POINT('Ctrl Pts',(-1.47579564172449,3.13432118289611,0.142181549535154));
#8798=CARTESIAN_POINT('Ctrl Pts',(-3.42956675747562,0.496557026061836,0.299320063048668));
#8799=CARTESIAN_POINT('Ctrl Pts',(-2.30343226514234,-2.58935922774548,0.456458576562181));
#8800=CARTESIAN_POINT('Ctrl Pts',(0.891761112414455,-3.34848577424617,0.613597090075694));
#8801=CARTESIAN_POINT('Ctrl Pts',(3.2859015926111,-1.1007252807108,0.770735603589207));
#8802=CARTESIAN_POINT('Ctrl Pts',(2.7288317609948,2.13597203247546,0.927874117102722));
#8803=CARTESIAN_POINT('Ctrl Pts',(-0.27919655644097,3.45406211813255,1.08501263061624));
#8804=CARTESIAN_POINT('Ctrl Pts',(-3.03644606033952,1.66993460430069,1.24215114412975));
#8805=CARTESIAN_POINT('Ctrl Pts',(-3.06648780987738,-1.61410638094873,1.39928965764326));
#8806=CARTESIAN_POINT('Ctrl Pts',(-0.342327145073366,-3.44839767949667,
1.55642817115678));
#8807=CARTESIAN_POINT('Ctrl Pts',(2.68929601578421,-2.18548654390084,1.71356668467029));
#8808=CARTESIAN_POINT('Ctrl Pts',(3.30550092715682,1.04034856780235,1.8707051981838));
#8809=CARTESIAN_POINT('Ctrl Pts',(0.952834920914103,3.33178039838987,2.02784371169731));
#8810=CARTESIAN_POINT('Ctrl Pts',(-2.25562944112346,2.630740466173,2.18498222521083));
#8811=CARTESIAN_POINT('Ctrl Pts',(-3.43817673987435,-0.433127500149091,
2.34212073872434));
#8812=CARTESIAN_POINT('Ctrl Pts',(-1.53268946892128,-3.10797698807607,2.49925925223786));
#8813=CARTESIAN_POINT('Ctrl Pts',(1.7493988709872,-2.99136460950407,2.65639776575137));
#8814=CARTESIAN_POINT('Ctrl Pts',(3.46024629894863,-0.188026617557356,2.81353627926488));
#8815=CARTESIAN_POINT('Ctrl Pts',(2.06323722577413,2.78418938435949,2.97067479277839));
#8816=CARTESIAN_POINT('Ctrl Pts',(-1.18688998506621,3.25575653825361,3.12781330629191));
#8817=CARTESIAN_POINT('Ctrl Pts',(-3.3709995165217,0.803131807227777,3.28495181980542));
#8818=CARTESIAN_POINT('Ctrl Pts',(-2.52741049074122,-2.37083416635282,3.44209033331894));
#8819=CARTESIAN_POINT('Ctrl Pts',(0.586198762341201,-3.41541058398195,3.59922884683245));
#8820=CARTESIAN_POINT('Ctrl Pts',(3.17330745213002,-1.3924001776803,3.75636736034597));
#8821=CARTESIAN_POINT('Ctrl Pts',(2.91027678633445,1.88120904397026,3.91350587385948));
#8822=CARTESIAN_POINT('Ctrl Pts',(0.0333505152943699,3.46519064195013,4.07064438737299));
#8823=CARTESIAN_POINT('Ctrl Pts',(-2.87352987075533,1.93687493734171,4.22778290088651));
#8824=CARTESIAN_POINT('Ctrl Pts',(-3.19951927885268,-1.33106529716661,4.38492141440001));
#8825=CARTESIAN_POINT('Ctrl Pts',(-0.651826904677972,-3.40349528097662,
4.54205992791353));
#8826=CARTESIAN_POINT('Ctrl Pts',(2.48131063733581,-2.41904029776201,4.69919844142705));
#8827=CARTESIAN_POINT('Ctrl Pts',(3.38583301773356,0.738101088738959,4.85633695494055));
#8828=CARTESIAN_POINT('Ctrl Pts',(1.24933397805696,3.23230924456058,5.01347546845408));
#8829=CARTESIAN_POINT('Ctrl Pts',(-2.00926747133911,2.82338496663079,5.17061398196758));
#8830=CARTESIAN_POINT('Ctrl Pts',(-3.46322427730269,-0.12139211787978,5.3277524954811));
#8831=CARTESIAN_POINT('Ctrl Pts',(-1.80664989208085,-2.95713959911133,5.48489100899462));
#8832=CARTESIAN_POINT('Ctrl Pts',(1.47258603363221,-3.13690114838409,5.64202952250812));
#8833=CARTESIAN_POINT('Ctrl Pts',(3.4292033754596,-0.499222045701823,5.79916803602164));
#8834=CARTESIAN_POINT('Ctrl Pts',(2.30584575575073,2.58683857089803,5.95630654953515));
#8835=CARTESIAN_POINT('Ctrl Pts',(-0.888531402702859,3.34950300605675,6.11344506304867));
#8836=CARTESIAN_POINT('Ctrl Pts',(-3.28486476693535,1.10377620199891,6.27058357656218));
#8837=CARTESIAN_POINT('Ctrl Pts',(-2.73086240406331,-2.13331876928079,6.4277220900757));
#8838=CARTESIAN_POINT('Ctrl Pts',(0.275892655912234,-3.45435112336383,6.5848606035892));
#8839=CARTESIAN_POINT('Ctrl Pts',(3.03485183459055,-1.67282180255638,6.74199911710273));
#8840=CARTESIAN_POINT('Ctrl Pts',(3.06802702248421,1.6111699572782,6.89913763061623));
#8841=CARTESIAN_POINT('Ctrl Pts',(0.345621576330127,3.44807252913389,7.05627614412975));
#8842=CARTESIAN_POINT('Ctrl Pts',(-2.68720751132516,2.18805261171336,7.21341465764325));
#8843=CARTESIAN_POINT('Ctrl Pts',(-3.30649300260574,-1.03718969811004,7.37055317115678));
#8844=CARTESIAN_POINT('Ctrl Pts',(-0.956017138014702,-3.33086920560938,
7.52769168467029));
#8845=CARTESIAN_POINT('Ctrl Pts',(2.25311553735071,-2.63289362024357,7.68483019818381));
#8846=CARTESIAN_POINT('Ctrl Pts',(3.43858888024395,0.429842977951538,7.84196871169731));
#8847=CARTESIAN_POINT('Ctrl Pts',(1.53565755714059,3.10651158777771,7.99910722521083));
#8848=CARTESIAN_POINT('Ctrl Pts',(-1.74654067132524,2.99303427005181,8.15624573872433));
#8849=CARTESIAN_POINT('Ctrl Pts',(-3.46006514069016,0.191331803382343,8.31338425223787));
#8850=CARTESIAN_POINT('Ctrl Pts',(-2.06589572612039,-2.78221724805058,8.47052276575136));
#8851=CARTESIAN_POINT('Ctrl Pts',(1.183779392948,-3.25688886436581,8.62766127926489));
#8852=CARTESIAN_POINT('Ctrl Pts',(3.37023102179748,-0.806351310370959,8.7847997927784));
#8853=CARTESIAN_POINT('Ctrl Pts',(2.52967359714463,2.36841856552378,8.94193830629191));
#8854=CARTESIAN_POINT('Ctrl Pts',(-0.582935293544439,3.41596954985013,9.09907681980542));
#8855=CARTESIAN_POINT('Ctrl Pts',(-3.17197740603666,1.3954296219005,9.25621533331893));
#8856=CARTESIAN_POINT('Ctrl Pts',(-2.91206965945989,-1.87842613074489,9.41335384683245));
#8857=CARTESIAN_POINT('Ctrl Pts',(-0.0366657672894424,-3.46516125435096,
9.57049236034596));
#8858=CARTESIAN_POINT('Ctrl Pts',(2.8716885037831,-1.93961114588268,9.72763087385947));
#8859=CARTESIAN_POINT('Ctrl Pts',(3.20077001198978,1.32799366090119,9.88476938737299));
#8860=CARTESIAN_POINT('Ctrl Pts',(0.655114493273841,3.40289939669598,10.0419079008865));
#8861=CARTESIAN_POINT('Ctrl Pts',(-2.47906919875826,2.42135526672317,10.1990464144));
#8862=CARTESIAN_POINT('Ctrl Pts',(-3.3864019310671,-0.734763106864168,10.3561849279135));
#8863=CARTESIAN_POINT('Ctrl Pts',(-1.25267830620767,-3.23131219035953,10.513323441427));
#8864=CARTESIAN_POINT('Ctrl Pts',(2.00706204302524,-2.82492459714601,10.6704619549406));
#8865=CARTESIAN_POINT('Ctrl Pts',(3.46239353138226,0.117358798249391,10.8276004684541));
#8866=CARTESIAN_POINT('Ctrl Pts',(1.81131357477516,2.9568147670617,10.9847389819676));
#8867=CARTESIAN_POINT('Ctrl Pts',(-1.47339811761136,3.13548357068097,11.1418774954811));
#8868=CARTESIAN_POINT('Ctrl Pts',(-2.77050414434575,1.38461669033425,11.2466365044901));
#8869=CARTESIAN_POINT('Ctrl Pts',(-2.91090525077877,0.426608275808828,11.2990160089946));
#8870=CARTESIAN_POINT('Ctrl Pts',(1.59774743137964,-2.24059110187414,-0.219489327336925));
#8871=CARTESIAN_POINT('Ctrl Pts',(2.33514866714022,-1.71475623207252,-0.167109822832421));
#8872=CARTESIAN_POINT('Ctrl Pts',(3.23863136773739,0.11226788144075,-0.0623508138234118));
#8873=CARTESIAN_POINT('Ctrl Pts',(1.6876604910601,2.76982094937113,0.0947876996901019));
#8874=CARTESIAN_POINT('Ctrl Pts',(-1.38044412748324,2.93181193130462,0.251926213203615));
#8875=CARTESIAN_POINT('Ctrl Pts',(-3.2079816177237,0.464474356210045,0.409064726717129));
#8876=CARTESIAN_POINT('Ctrl Pts',(-2.15460694798876,-2.42206010021071,0.566203240230643));
#8877=CARTESIAN_POINT('Ctrl Pts',(0.834144210720117,-3.13213929648004,0.723341753744155));
#8878=CARTESIAN_POINT('Ctrl Pts',(3.07359869399491,-1.02960715343621,0.880480267257669));
#8879=CARTESIAN_POINT('Ctrl Pts',(2.55252127926951,1.99796636155783,1.03761878077118));
#8880=CARTESIAN_POINT('Ctrl Pts',(-0.261157599233816,3.2308943271893,1.19475729428469));
#8881=CARTESIAN_POINT('Ctrl Pts',(-2.84026054414775,1.56203972461538,1.35189580779821));
#8882=CARTESIAN_POINT('Ctrl Pts',(-2.86836128896387,-1.50981857631063,1.50903432131172));
#8883=CARTESIAN_POINT('Ctrl Pts',(-0.320209305227662,-3.22559586930712,
1.66617283482524));
#8884=CARTESIAN_POINT('Ctrl Pts',(2.51553994814305,-2.04428172839443,1.82331134833875));
#8885=CARTESIAN_POINT('Ctrl Pts',(3.09193171078347,0.973131394588079,1.98044986185226));
#8886=CARTESIAN_POINT('Ctrl Pts',(0.891272025644291,3.1165132590083,2.13758837536578));
#8887=CARTESIAN_POINT('Ctrl Pts',(-2.10989267602029,2.4607676867899,2.29472688887929));
#8888=CARTESIAN_POINT('Ctrl Pts',(-3.21603530707201,-0.405143027346019,
2.4518654023928));
#8889=CARTESIAN_POINT('Ctrl Pts',(-1.43366203071003,-2.90716984129947,2.60900391590632));
#8890=CARTESIAN_POINT('Ctrl Pts',(1.63636978576396,-2.79809181678146,2.76614242941983));
#8891=CARTESIAN_POINT('Ctrl Pts',(3.23667894658341,-0.175878172207005,2.92328094293335));
#8892=CARTESIAN_POINT('Ctrl Pts',(1.92993096835312,2.60430223316632,3.08041945644686));
#8893=CARTESIAN_POINT('Ctrl Pts',(-1.11020473535129,3.04540131890859,3.23755796996037));
#8894=CARTESIAN_POINT('Ctrl Pts',(-3.15319842040834,0.751241266431068,3.39469648347389));
#8895=CARTESIAN_POINT('Ctrl Pts',(-2.36411388612472,-2.21765399601942,3.5518349969874));
#8896=CARTESIAN_POINT('Ctrl Pts',(0.548324318173406,-3.19474007803184,3.70897351050091));
#8897=CARTESIAN_POINT('Ctrl Pts',(2.96827928823051,-1.30243686459143,3.86611202401443));
#8898=CARTESIAN_POINT('Ctrl Pts',(2.72224309752783,1.75966367151117,4.02325053752794));
#8899=CARTESIAN_POINT('Ctrl Pts',(0.0311957304148393,3.24130383438475,4.18038905104146));
#8900=CARTESIAN_POINT('Ctrl Pts',(-2.68787040907414,1.81173297801481,4.33752756455496));
#8901=CARTESIAN_POINT('Ctrl Pts',(-2.99279756247315,-1.24506484557935,4.49466607806848));
#8902=CARTESIAN_POINT('Ctrl Pts',(-0.609712210321215,-3.18359462564273,
4.65180459158199));
#8903=CARTESIAN_POINT('Ctrl Pts',(2.32099255542547,-2.26274551758992,4.80894310509551));
#8904=CARTESIAN_POINT('Ctrl Pts',(3.16707352551029,0.69041219843154,4.96608161860902));
#8905=CARTESIAN_POINT('Ctrl Pts',(1.16861420681437,3.02346896054623,5.12322013212254));
#8906=CARTESIAN_POINT('Ctrl Pts',(-1.87944821283798,2.64096537936348,5.28035864563605));
#8907=CARTESIAN_POINT('Ctrl Pts',(-3.23946451703395,-0.113548943710187,
5.43749715914956));
#8908=CARTESIAN_POINT('Ctrl Pts',(-1.68992180450333,-2.76607809260859,5.59463567266307));
#8909=CARTESIAN_POINT('Ctrl Pts',(1.37744189294803,-2.93422520459686,5.75177418617659));
#8910=CARTESIAN_POINT('Ctrl Pts',(3.20764171390784,-0.466967188284919,5.9089126996901));
#8911=CARTESIAN_POINT('Ctrl Pts',(2.15686450238375,2.41970230361335,6.06605121320362));
#8912=CARTESIAN_POINT('Ctrl Pts',(-0.831123173336083,3.13309080469669,6.22318972671712));
#8913=CARTESIAN_POINT('Ctrl Pts',(-3.07262885787747,1.03246095396017,6.38032824023064));
#8914=CARTESIAN_POINT('Ctrl Pts',(-2.55442072199701,-1.99548452634149,6.53746675374416));
#8915=CARTESIAN_POINT('Ctrl Pts',(0.258067164519323,-3.23116465972251,6.69460526725767));
#8916=CARTESIAN_POINT('Ctrl Pts',(2.83876932171097,-1.56474038029172,6.85174378077119));
#8917=CARTESIAN_POINT('Ctrl Pts',(2.86980105267096,1.50707187568543,7.00888229428469));
#8918=CARTESIAN_POINT('Ctrl Pts',(0.323290882482136,3.22529172698812,7.1660208077982));
#8919=CARTESIAN_POINT('Ctrl Pts',(-2.51358638246349,2.04668200194341,7.32315932131173));
#8920=CARTESIAN_POINT('Ctrl Pts',(-3.09285968799709,-0.970176620232505,
7.48029783482524));
#8921=CARTESIAN_POINT('Ctrl Pts',(-0.89424863892644,-3.11566093861428,7.63743634833875));
#8922=CARTESIAN_POINT('Ctrl Pts',(2.10754119617984,-2.46278172505391,7.79457486185227));
#8923=CARTESIAN_POINT('Ctrl Pts',(3.21642081895241,0.402070718924034,7.95171337536577));
#8924=CARTESIAN_POINT('Ctrl Pts',(1.43643835002984,2.90579912086969,8.1088518888793));
#8925=CARTESIAN_POINT('Ctrl Pts',(-1.63369625507517,2.79965360015637,8.2659904023928));
#8926=CARTESIAN_POINT('Ctrl Pts',(-3.23650949300394,0.178969809174445,8.42312891590632));
#8927=CARTESIAN_POINT('Ctrl Pts',(-1.93241770234741,-2.6024575170625,8.58026742941983));
#8928=CARTESIAN_POINT('Ctrl Pts',(1.10729511934404,-3.04646048515613,8.73740594293334));
#8929=CARTESIAN_POINT('Ctrl Pts',(3.15247957831459,-0.75425275669555,8.89454445644686));
#8930=CARTESIAN_POINT('Ctrl Pts',(2.36623077267467,2.21539446774564,9.05168296996036));
#8931=CARTESIAN_POINT('Ctrl Pts',(-0.54527170288688,3.19526292897974,9.20882148347389));
#8932=CARTESIAN_POINT('Ctrl Pts',(-2.96703517673773,1.30527057568604,9.36595999698739));
#8933=CARTESIAN_POINT('Ctrl Pts',(-2.72392013268591,-1.75706056298405,9.52309851050092));
#8934=CARTESIAN_POINT('Ctrl Pts',(-0.0342967831746755,-3.24127634552548,
9.68023702401442));
#8935=CARTESIAN_POINT('Ctrl Pts',(2.68614801326846,-1.81429239945851,9.83737553752795));
#8936=CARTESIAN_POINT('Ctrl Pts',(2.99396748543899,1.24219166847781,9.99451405104144));
#8937=CARTESIAN_POINT('Ctrl Pts',(0.612787387020777,3.18303724158995,10.151652564555));
#8938=CARTESIAN_POINT('Ctrl Pts',(-2.31889593673789,2.2649109158452,10.3087910780685));
#8939=CARTESIAN_POINT('Ctrl Pts',(-3.16760568121541,-0.687289884375024,
10.465929591582));
#8940=CARTESIAN_POINT('Ctrl Pts',(-1.17174245711238,-3.02253632625886,10.6230681050955));
#8941=CARTESIAN_POINT('Ctrl Pts',(1.8773852777822,-2.64240553397781,10.780206618609));
#8942=CARTESIAN_POINT('Ctrl Pts',(3.23868744580887,0.109776217839061,10.9373451321225));
#8943=CARTESIAN_POINT('Ctrl Pts',(1.69428416552798,2.76577424803644,11.0944836456361));
#8944=CARTESIAN_POINT('Ctrl Pts',(-1.37820150798437,2.93289921693286,11.2516221591496));
#8945=CARTESIAN_POINT('Ctrl Pts',(-2.59150119982806,1.29515627025004,11.3563811681586));
#8946=CARTESIAN_POINT('Ctrl Pts',(-2.72283095673203,0.399045011671044,11.4087606726631));
#8947=CARTESIAN_POINT('Ctrl Pts',(1.48738611075532,-2.08582659521589,-0.109744663668464));
#8948=CARTESIAN_POINT('Ctrl Pts',(2.17385277913045,-1.59631275433404,-0.0573651591639592));
#8949=CARTESIAN_POINT('Ctrl Pts',(3.01492915564857,0.104513194175331,0.0473938498450494));
#8950=CARTESIAN_POINT('Ctrl Pts',(1.57108859934498,2.57850091226017,0.204532363358563));
#8951=CARTESIAN_POINT('Ctrl Pts',(-1.28509261324199,2.72930267971312,0.361670876872076));
#8952=CARTESIAN_POINT('Ctrl Pts',(-2.98639647797178,0.432391686358259,0.51880939038559));
#8953=CARTESIAN_POINT('Ctrl Pts',(-2.00578163083517,-2.25476097267596,0.675947903899103));
#8954=CARTESIAN_POINT('Ctrl Pts',(0.776527309025778,-2.9157928187139,0.833086417412617));
#8955=CARTESIAN_POINT('Ctrl Pts',(2.86129579537873,-0.958489026161636,0.99022493092613));
#8956=CARTESIAN_POINT('Ctrl Pts',(2.37621079754423,1.85996069064019,1.14736344443964));
#8957=CARTESIAN_POINT('Ctrl Pts',(-0.243118642026661,3.00772653624605,1.30450195795316));
#8958=CARTESIAN_POINT('Ctrl Pts',(-2.64407502795598,1.45414484493007,1.46164047146667));
#8959=CARTESIAN_POINT('Ctrl Pts',(-2.67023476805036,-1.40553077167252,1.61877898498018));
#8960=CARTESIAN_POINT('Ctrl Pts',(-0.298091465381954,-3.00279405911757,
1.7759174984937));
#8961=CARTESIAN_POINT('Ctrl Pts',(2.34178388050189,-1.90307691288803,1.93305601200721));
#8962=CARTESIAN_POINT('Ctrl Pts',(2.87836249441012,0.905914221373807,2.09019452552073));
#8963=CARTESIAN_POINT('Ctrl Pts',(0.829709130374474,2.90124611962672,2.24733303903424));
#8964=CARTESIAN_POINT('Ctrl Pts',(-1.96415591091712,2.2907949074068,2.40447155254775));
#8965=CARTESIAN_POINT('Ctrl Pts',(-2.99389387426969,-0.37715855454295,2.56161006606126));
#8966=CARTESIAN_POINT('Ctrl Pts',(-1.33463459249878,-2.70636269452286,2.71874857957478));
#8967=CARTESIAN_POINT('Ctrl Pts',(1.52334070054072,-2.60481902405885,2.87588709308829));
#8968=CARTESIAN_POINT('Ctrl Pts',(3.01311159421818,-0.163729726856653,3.03302560660181));
#8969=CARTESIAN_POINT('Ctrl Pts',(1.79662471093212,2.42441508197314,3.19016412011532));
#8970=CARTESIAN_POINT('Ctrl Pts',(-1.03351948563637,2.83504609956357,3.34730263362884));
#8971=CARTESIAN_POINT('Ctrl Pts',(-2.93539732429499,0.699350725634357,3.50444114714234));
#8972=CARTESIAN_POINT('Ctrl Pts',(-2.20081728150821,-2.06447382568602,3.66157966065586));
#8973=CARTESIAN_POINT('Ctrl Pts',(0.510449874005612,-2.97406957208172,3.81871817416937));
#8974=CARTESIAN_POINT('Ctrl Pts',(2.763251124331,-1.21247355150257,3.97585668768289));
#8975=CARTESIAN_POINT('Ctrl Pts',(2.5342094087212,1.63811829905208,4.1329952011964));
#8976=CARTESIAN_POINT('Ctrl Pts',(0.029040945535309,3.01741702681936,4.29013371470992));
#8977=CARTESIAN_POINT('Ctrl Pts',(-2.50221094739296,1.68659101868791,4.44727222822342));
#8978=CARTESIAN_POINT('Ctrl Pts',(-2.78607584609361,-1.1590643939921,4.60441074173694));
#8979=CARTESIAN_POINT('Ctrl Pts',(-0.56759751596446,-2.96369397030884,4.76154925525046));
#8980=CARTESIAN_POINT('Ctrl Pts',(2.16067447351513,-2.10645073741783,4.91868776876396));
#8981=CARTESIAN_POINT('Ctrl Pts',(2.94831403328702,0.642723308124124,5.07582628227749));
#8982=CARTESIAN_POINT('Ctrl Pts',(1.08789443557179,2.81462867653188,5.23296479579099));
#8983=CARTESIAN_POINT('Ctrl Pts',(-1.74962895433684,2.45854579209617,5.39010330930451));
#8984=CARTESIAN_POINT('Ctrl Pts',(-3.01570475676522,-0.105705769540595,
5.54724182281802));
#8985=CARTESIAN_POINT('Ctrl Pts',(-1.57319371692581,-2.57501658610585,5.70438033633154));
#8986=CARTESIAN_POINT('Ctrl Pts',(1.28229775226384,-2.73154926080963,5.86151884984505));
#8987=CARTESIAN_POINT('Ctrl Pts',(2.98608005235609,-0.434712330868017,6.01865736335856));
#8988=CARTESIAN_POINT('Ctrl Pts',(2.00788324901678,2.25256603632868,6.17579587687208));
#8989=CARTESIAN_POINT('Ctrl Pts',(-0.773714943969305,2.91667860333663,6.33293439038559));
#8990=CARTESIAN_POINT('Ctrl Pts',(-2.86039294881959,0.961145705921419,6.4900729038991));
#8991=CARTESIAN_POINT('Ctrl Pts',(-2.37797903993071,-1.85765028340219,6.64721141741262));
#8992=CARTESIAN_POINT('Ctrl Pts',(0.240241673126412,-3.0079781960812,6.80434993092612));
#8993=CARTESIAN_POINT('Ctrl Pts',(2.64268680883139,-1.45665895802706,6.96148844443965));
#8994=CARTESIAN_POINT('Ctrl Pts',(2.67157508285772,1.40297379409266,7.11862695795316));
#8995=CARTESIAN_POINT('Ctrl Pts',(0.300960188634146,3.00251092484234,7.27576547146667));
#8996=CARTESIAN_POINT('Ctrl Pts',(-2.33996525360183,1.90531139217345,7.43290398498018));
#8997=CARTESIAN_POINT('Ctrl Pts',(-2.87922637338843,-0.903163542354968,
7.5900424984937));
#8998=CARTESIAN_POINT('Ctrl Pts',(-0.832480139838179,-2.90045267161919,
7.74718101200721));
#8999=CARTESIAN_POINT('Ctrl Pts',(1.96196685500896,-2.29266982986425,7.90431952552073));
#9000=CARTESIAN_POINT('Ctrl Pts',(2.99425275766087,0.37429845989653,8.06145803903424));
#9001=CARTESIAN_POINT('Ctrl Pts',(1.33721914291908,2.70508665396167,8.21859655254775));
#9002=CARTESIAN_POINT('Ctrl Pts',(-1.5208518388251,2.60627293026094,8.37573506606126));
#9003=CARTESIAN_POINT('Ctrl Pts',(-3.01295384531772,0.166607814966547,8.53287357957478));
#9004=CARTESIAN_POINT('Ctrl Pts',(-1.79893967857444,-2.42269778607442,8.69001209308829));
#9005=CARTESIAN_POINT('Ctrl Pts',(1.03081084574009,-2.83603210594645,8.8471506066018));
#9006=CARTESIAN_POINT('Ctrl Pts',(2.9347281348317,-0.702154203020143,9.00428912011532));
#9007=CARTESIAN_POINT('Ctrl Pts',(2.20278794820472,2.06237036996751,9.16142763362883));
#9008=CARTESIAN_POINT('Ctrl Pts',(-0.507608112229325,2.97455630810935,9.31856614714235));
#9009=CARTESIAN_POINT('Ctrl Pts',(-2.7620929474388,1.21511152947157,9.47570466065586));
#9010=CARTESIAN_POINT('Ctrl Pts',(-2.53577060591194,-1.63569499522321,9.63284317416937));
#9011=CARTESIAN_POINT('Ctrl Pts',(-0.0319277990599106,-3.0173914367,9.78998168768289));
#9012=CARTESIAN_POINT('Ctrl Pts',(2.50060752275382,-1.68897365303435,9.94712020119639));
#9013=CARTESIAN_POINT('Ctrl Pts',(2.78716495888821,1.15638967605443,10.1042587147099));
#9014=CARTESIAN_POINT('Ctrl Pts',(0.570460280767717,2.96317508648391,10.2613972282234));
#9015=CARTESIAN_POINT('Ctrl Pts',(-2.15872267471752,2.10846656496723,10.4185357417369));
#9016=CARTESIAN_POINT('Ctrl Pts',(-2.94880943136371,-0.639816661885883,
10.5756742552505));
#9017=CARTESIAN_POINT('Ctrl Pts',(-1.09080660801709,-2.8137604621582,10.732812768764));
#9018=CARTESIAN_POINT('Ctrl Pts',(1.74770851253917,-2.4598864708096,10.8899512822775));
#9019=CARTESIAN_POINT('Ctrl Pts',(3.01498136023548,0.102193637428725,11.047089795791));
#9020=CARTESIAN_POINT('Ctrl Pts',(1.57725475628079,2.57473372901119,11.2042283093045));
#9021=CARTESIAN_POINT('Ctrl Pts',(-1.28300489835739,2.73031486318474,11.361366822818));
#9022=CARTESIAN_POINT('Ctrl Pts',(-2.41249825531037,1.20569585016584,11.466125831827));
#9023=CARTESIAN_POINT('Ctrl Pts',(-2.53475666268528,0.371481747533259,11.5185053363315));
#9024=CARTESIAN_POINT('Ctrl Pts',(1.37702479013101,-1.93106208855765,-2.4980018054066E-15));
#9025=CARTESIAN_POINT('Ctrl Pts',(2.01255689112068,-1.47786927659557,0.052379504504502));
#9026=CARTESIAN_POINT('Ctrl Pts',(2.79122694355976,0.0967585069099138,0.157138513513511));
#9027=CARTESIAN_POINT('Ctrl Pts',(1.45451670762985,2.3871808751492,0.314277027027025));
#9028=CARTESIAN_POINT('Ctrl Pts',(-1.18974109900074,2.52679342812162,0.471415540540538));
#9029=CARTESIAN_POINT('Ctrl Pts',(-2.76481133821986,0.40030901650647,0.628554054054051));
#9030=CARTESIAN_POINT('Ctrl Pts',(-1.85695631368159,-2.0874618451412,0.785692567567565));
#9031=CARTESIAN_POINT('Ctrl Pts',(0.718910407331439,-2.69944634094777,0.942831081081078));
#9032=CARTESIAN_POINT('Ctrl Pts',(2.64899289676255,-0.887370898887054,1.09996959459459));
#9033=CARTESIAN_POINT('Ctrl Pts',(2.19990031581894,1.72195501972256,1.25710810810811));
#9034=CARTESIAN_POINT('Ctrl Pts',(-0.225079684819506,2.78455874530281,1.41424662162162));
#9035=CARTESIAN_POINT('Ctrl Pts',(-2.44788951176421,1.34624996524475,1.57138513513514));
#9036=CARTESIAN_POINT('Ctrl Pts',(-2.47210824713685,-1.30124296703442,1.72852364864864));
#9037=CARTESIAN_POINT('Ctrl Pts',(-0.275973625536248,-2.77999224892802,
1.88566216216216));
#9038=CARTESIAN_POINT('Ctrl Pts',(2.16802781286073,-1.76187209738162,2.04280067567567));
#9039=CARTESIAN_POINT('Ctrl Pts',(2.66479327803676,0.838697048159531,2.19993918918919));
#9040=CARTESIAN_POINT('Ctrl Pts',(0.76814623510466,2.68597898024514,2.3570777027027));
#9041=CARTESIAN_POINT('Ctrl Pts',(-1.81841914581395,2.1208221280237,2.51421621621621));
#9042=CARTESIAN_POINT('Ctrl Pts',(-2.77175244146736,-0.349174081739879,
2.67135472972972));
#9043=CARTESIAN_POINT('Ctrl Pts',(-1.23560715428754,-2.50555554774625,2.82849324324324));
#9044=CARTESIAN_POINT('Ctrl Pts',(1.41031161531747,-2.41154623133624,2.98563175675675));
#9045=CARTESIAN_POINT('Ctrl Pts',(2.78954424185296,-0.151581281506301,3.14277027027027));
#9046=CARTESIAN_POINT('Ctrl Pts',(1.66331845351111,2.24452793077997,3.29990878378378));
#9047=CARTESIAN_POINT('Ctrl Pts',(-0.956834235921451,2.62469088021855,3.45704729729729));
#9048=CARTESIAN_POINT('Ctrl Pts',(-2.71759622818163,0.647460184837647,3.61418581081081));
#9049=CARTESIAN_POINT('Ctrl Pts',(-2.03752067689171,-1.91129365535261,3.77132432432432));
#9050=CARTESIAN_POINT('Ctrl Pts',(0.47257542983782,-2.75339906613161,3.92846283783783));
#9051=CARTESIAN_POINT('Ctrl Pts',(2.55822296043148,-1.12251023841371,4.08560135135135));
#9052=CARTESIAN_POINT('Ctrl Pts',(2.34617571991457,1.51657292659299,4.24273986486486));
#9053=CARTESIAN_POINT('Ctrl Pts',(0.0268861606557786,2.79353021925399,4.39987837837838));
#9054=CARTESIAN_POINT('Ctrl Pts',(-2.31655148571177,1.56144905936101,4.55701689189189));
#9055=CARTESIAN_POINT('Ctrl Pts',(-2.57935412971408,-1.07306394240484,4.7141554054054));
#9056=CARTESIAN_POINT('Ctrl Pts',(-0.525482821607704,-2.74379331497496,
4.87129391891892));
#9057=CARTESIAN_POINT('Ctrl Pts',(2.00035639160479,-1.95015595724574,5.02843243243243));
#9058=CARTESIAN_POINT('Ctrl Pts',(2.72955454106374,0.595034417816705,5.18557094594594));
#9059=CARTESIAN_POINT('Ctrl Pts',(1.0071746643292,2.60578839251754,5.34270945945947));
#9060=CARTESIAN_POINT('Ctrl Pts',(-1.61980969583571,2.27612620482886,5.49984797297296));
#9061=CARTESIAN_POINT('Ctrl Pts',(-2.79194499649648,-0.0978625953710016,
5.6569864864865));
#9062=CARTESIAN_POINT('Ctrl Pts',(-1.45646562934828,-2.38395507960311,5.81412499999999));
#9063=CARTESIAN_POINT('Ctrl Pts',(1.18715361157964,-2.5288733170224,5.97126351351352));
#9064=CARTESIAN_POINT('Ctrl Pts',(2.76451839080433,-0.402457473451116,6.12840202702702));
#9065=CARTESIAN_POINT('Ctrl Pts',(1.8589019956498,2.08542976904401,6.28554054054054));
#9066=CARTESIAN_POINT('Ctrl Pts',(-0.716306714602523,2.70026640197657,6.44267905405405));
#9067=CARTESIAN_POINT('Ctrl Pts',(-2.64815703976171,0.889830457882673,6.59981756756756));
#9068=CARTESIAN_POINT('Ctrl Pts',(-2.20153735786441,-1.71981604046289,6.75695608108108));
#9069=CARTESIAN_POINT('Ctrl Pts',(0.222416181733502,-2.78479173243988,6.91409459459459));
#9070=CARTESIAN_POINT('Ctrl Pts',(2.4466042959518,-1.34857753576241,7.0712331081081));
#9071=CARTESIAN_POINT('Ctrl Pts',(2.47334911304448,1.29887571249989,7.22837162162162));
#9072=CARTESIAN_POINT('Ctrl Pts',(0.278629494786153,2.77973012269657,7.38551013513513));
#9073=CARTESIAN_POINT('Ctrl Pts',(-2.16634412474015,1.76394078240349,7.54264864864865));
#9074=CARTESIAN_POINT('Ctrl Pts',(-2.66559305877978,-0.83615046447743,7.69978716216215));
#9075=CARTESIAN_POINT('Ctrl Pts',(-0.770711640749916,-2.68524440462409,
7.85692567567567));
#9076=CARTESIAN_POINT('Ctrl Pts',(1.81639251383808,-2.12255793467458,8.01406418918919));
#9077=CARTESIAN_POINT('Ctrl Pts',(2.77208469636934,0.346526200869026,8.1712027027027));
#9078=CARTESIAN_POINT('Ctrl Pts',(1.23799993580832,2.50437418705365,8.32834121621622));
#9079=CARTESIAN_POINT('Ctrl Pts',(-1.40800742257503,2.4128922603655,8.48547972972973));
#9080=CARTESIAN_POINT('Ctrl Pts',(-2.78939819763151,0.154245820758651,8.64261824324324));
#9081=CARTESIAN_POINT('Ctrl Pts',(-1.66546165480147,-2.24293805508635,8.79975675675676));
#9082=CARTESIAN_POINT('Ctrl Pts',(0.954326572136137,-2.62560372673677,8.95689527027026));
#9083=CARTESIAN_POINT('Ctrl Pts',(2.71697669134881,-0.650055649344734,9.11403378378378));
#9084=CARTESIAN_POINT('Ctrl Pts',(2.03934512373477,1.90934627218937,9.2711722972973));
#9085=CARTESIAN_POINT('Ctrl Pts',(-0.469944521571767,2.75384968723896,9.42831081081079));
#9086=CARTESIAN_POINT('Ctrl Pts',(-2.55715071813987,1.12495248325711,9.58544932432433));
#9087=CARTESIAN_POINT('Ctrl Pts',(-2.34762107913798,-1.51432942746238,9.74258783783783));
#9088=CARTESIAN_POINT('Ctrl Pts',(-0.0295588149451427,-2.79350652787453,
9.89972635135136));
#9089=CARTESIAN_POINT('Ctrl Pts',(2.31506703223917,-1.56365490661018,10.0568648648649));
#9090=CARTESIAN_POINT('Ctrl Pts',(2.58036243233743,1.07058768363104,10.2140033783784));
#9091=CARTESIAN_POINT('Ctrl Pts',(0.528133174514654,2.74331293137788,10.3711418918919));
#9092=CARTESIAN_POINT('Ctrl Pts',(-1.99854941269714,1.95202221408926,10.5282804054054));
#9093=CARTESIAN_POINT('Ctrl Pts',(-2.73001318151202,-0.59234343939674,10.6854189189189));
#9094=CARTESIAN_POINT('Ctrl Pts',(-1.0098707589218,-2.60498459805753,10.8425574324324));
#9095=CARTESIAN_POINT('Ctrl Pts',(1.61803174729613,-2.2773674076414,10.999695945946));
#9096=CARTESIAN_POINT('Ctrl Pts',(2.79127527466209,0.0946110570183949,11.1568344594594));
#9097=CARTESIAN_POINT('Ctrl Pts',(1.46022534703361,2.38369320998594,11.313972972973));
#9098=CARTESIAN_POINT('Ctrl Pts',(-1.1878082887304,2.52773050943662,11.4711114864865));
#9099=CARTESIAN_POINT('Ctrl Pts',(-2.23349531079268,1.11623543008163,11.5758704954955));
#9100=CARTESIAN_POINT('Ctrl Pts',(-2.34668236863853,0.343918483395475,11.62825));
#9101=CARTESIAN_POINT('',(1.37702479013102,-1.93106208855765,0.));
#9102=CARTESIAN_POINT('Ctrl Pts',(1.37702479013101,-1.93106208855765,-2.4980018054066E-15));
#9103=CARTESIAN_POINT('Ctrl Pts',(2.01255689112068,-1.47786927659557,0.052379504504502));
#9104=CARTESIAN_POINT('Ctrl Pts',(2.79122694355976,0.0967585069099138,0.157138513513511));
#9105=CARTESIAN_POINT('Ctrl Pts',(1.45451670762985,2.3871808751492,0.314277027027025));
#9106=CARTESIAN_POINT('Ctrl Pts',(-1.18974109900074,2.52679342812162,0.471415540540538));
#9107=CARTESIAN_POINT('Ctrl Pts',(-2.31615344009055,1.00603694073732,0.583793234229858));
#9108=CARTESIAN_POINT('Ctrl Pts',(-2.37458477423974,0.11510370689526,0.643791423414673));
#9109=CARTESIAN_POINT('Ctrl Pts',(-2.37366757034868,0.001844716469488,0.651410108094984));
#9110=CARTESIAN_POINT('Ctrl Pts',(1.29197400994444,2.64783394680711,-2.46330733588707E-16));
#9111=CARTESIAN_POINT('Ctrl Pts',(1.37074936016223,2.60046826619745,-2.90204607120186E-16));
#9112=CARTESIAN_POINT('Ctrl Pts',(1.44700091320012,2.54930204226795,-5.92854700626308E-16));
#9113=CARTESIAN_POINT('Ctrl Pts',(1.5204041597113,2.49432533414619,-4.68375338513738E-16));
#9114=CARTESIAN_POINT('Ctrl Pts',(1.59876972116939,2.43563200920691,-3.1748808003354E-16));
#9115=CARTESIAN_POINT('Ctrl Pts',(1.67388955782072,2.37259497158855,9.42702435984343E-17));
#9116=CARTESIAN_POINT('Ctrl Pts',(1.74558455766593,2.30559334150577,2.91433543964104E-16));
#9117=CARTESIAN_POINT('Ctrl Pts',(1.78514524738377,2.26862241321206,4.00226572297347E-16));
#9118=CARTESIAN_POINT('Ctrl Pts',(1.82366240526687,2.23044382157621,2.41712413072573E-16));
#9119=CARTESIAN_POINT('Ctrl Pts',(1.86109995619813,2.19111823230724,2.56739074444567E-16));
#9120=CARTESIAN_POINT('Ctrl Pts',(1.87813922122651,2.17321964863167,2.63578284255041E-16));
#9121=CARTESIAN_POINT('Ctrl Pts',(1.89495840460327,2.15507923207588,-5.32738877742354E-17));
#9122=CARTESIAN_POINT('Ctrl Pts',(1.91153266312519,2.13672660521873,-9.0205620750794E-17));
#9123=CARTESIAN_POINT('Ctrl Pts',(1.97664662778045,2.0646261070319,-2.35296368099375E-16));
#9124=CARTESIAN_POINT('Ctrl Pts',(2.03804038590891,1.98919650283574,-3.72373475267393E-16));
#9125=CARTESIAN_POINT('Ctrl Pts',(2.09554796148623,1.91081666271006,-8.32667268468867E-17));
#9126=CARTESIAN_POINT('Ctrl Pts',(2.14343533270609,1.8455486617107,1.57476549926517E-16));
#9127=CARTESIAN_POINT('Ctrl Pts',(2.18862729734747,1.77823406218829,2.53857300975798E-16));
#9128=CARTESIAN_POINT('Ctrl Pts',(2.23100237945407,1.70908145885149,3.19189119579733E-16));
#9129=CARTESIAN_POINT('Ctrl Pts',(2.2495414778757,1.67882719489164,3.47771790218954E-16));
#9130=CARTESIAN_POINT('Ctrl Pts',(2.26754109313608,1.64822104628506,2.94521883274651E-16));
#9131=CARTESIAN_POINT('Ctrl Pts',(2.28498954152194,1.61728023964544,3.19189119579733E-16));
#9132=CARTESIAN_POINT('Ctrl Pts',(2.29543189661598,1.59876312668031,3.33951695310829E-16));
#9133=CARTESIAN_POINT('Ctrl Pts',(2.30567682494647,1.58012614919259,-6.61366324171955E-18));
#9134=CARTESIAN_POINT('Ctrl Pts',(2.31572165746038,1.56137299470242,-1.38777878078145E-17));
#9135=CARTESIAN_POINT('Ctrl Pts',(2.32292320728395,1.54792809393149,-1.90857347710862E-17));
#9136=CARTESIAN_POINT('Ctrl Pts',(2.33002152872364,1.53442403232929,-1.12870283643031E-16));
#9137=CARTESIAN_POINT('Ctrl Pts',(2.33700969851763,1.52087413145422,-1.11022302462516E-16));
#9138=CARTESIAN_POINT('Ctrl Pts',(2.38058260792534,1.43638725996736,-9.94996979838631E-17));
#9139=CARTESIAN_POINT('Ctrl Pts',(2.41994184512486,1.3499998824768,-3.77842799305168E-16));
#9140=CARTESIAN_POINT('Ctrl Pts',(2.45492973401008,1.26206183108408,-3.7470027081099E-16));
#9141=CARTESIAN_POINT('Ctrl Pts',(2.48961375478266,1.17488751738912,-3.71585035023886E-16));
#9142=CARTESIAN_POINT('Ctrl Pts',(2.52000223755862,1.08618841594484,-4.13121512185277E-16));
#9143=CARTESIAN_POINT('Ctrl Pts',(2.54589150534161,0.996296170221892,-3.7470027081099E-16));
#9144=CARTESIAN_POINT('Ctrl Pts',(2.57095558696702,0.909269120898709,-3.37503655671981E-16));
#9145=CARTESIAN_POINT('Ctrl Pts',(2.59180267862827,0.821123009321661,-1.98135956264892E-16));
#9146=CARTESIAN_POINT('Ctrl Pts',(2.60819974692058,0.732162501184589,-2.77555756156289E-16));
#9147=CARTESIAN_POINT('Ctrl Pts',(2.61796168819389,0.679200152025794,-3.24838075693952E-16));
#9148=CARTESIAN_POINT('Ctrl Pts',(2.62614545111416,0.625949276096869,-2.51374357035676E-17));
#9149=CARTESIAN_POINT('Ctrl Pts',(2.63269335080009,0.572476447093945,0.));
#9150=CARTESIAN_POINT('Ctrl Pts',(2.6352683765624,0.5514477327168,9.88554309620052E-18));
#9151=CARTESIAN_POINT('Ctrl Pts',(2.63759088070415,0.530377846603737,-5.43523939458827E-17));
#9152=CARTESIAN_POINT('Ctrl Pts',(2.63965388200594,0.50930758122065,-2.77555756156289E-17));
#9153=CARTESIAN_POINT('Ctrl Pts',(2.64834931960739,0.420497565576959,8.43485582923526E-17));
#9154=CARTESIAN_POINT('Ctrl Pts',(2.65245297898025,0.3315870178655,7.13394232030532E-17));
#9155=CARTESIAN_POINT('Ctrl Pts',(2.65178792227632,0.242870082265014,1.11022302462516E-16));
#9156=CARTESIAN_POINT('Ctrl Pts',(2.65141677862428,0.193360428001277,1.33167855834344E-16));
#9157=CARTESIAN_POINT('Ctrl Pts',(2.64955959473733,0.143911103160085,2.55410202784461E-16));
#9158=CARTESIAN_POINT('Ctrl Pts',(2.64617859082989,0.0945743399740305,2.77555756156289E-16));
#9159=CARTESIAN_POINT('Ctrl Pts',(2.63998980161557,0.00426541509996067,
2.91350122435194E-16));
#9160=CARTESIAN_POINT('Ctrl Pts',(2.62869784498548,-0.0856678806083358,
1.22336690906674E-16));
#9161=CARTESIAN_POINT('Ctrl Pts',(2.61249699286393,-0.174890907412304,1.94289029309402E-16));
#9162=CARTESIAN_POINT('Ctrl Pts',(2.59606370990205,-0.265394001643718,2.67273655542046E-16));
#9163=CARTESIAN_POINT('Ctrl Pts',(2.57457910556097,-0.355167245076682,-8.63540186836622E-17));
#9164=CARTESIAN_POINT('Ctrl Pts',(2.54820206281091,-0.443829678011398,-1.94289029309402E-16));
#9165=CARTESIAN_POINT('Ctrl Pts',(2.5433159398537,-0.460253640057088,-2.14283072550056E-16));
#9166=CARTESIAN_POINT('Ctrl Pts',(2.53826078384047,-0.476642310793062,2.54370247567095E-16));
#9167=CARTESIAN_POINT('Ctrl Pts',(2.53304532831965,-0.49296952041645,2.4980018054066E-16));
#9168=CARTESIAN_POINT('Ctrl Pts',(2.5060606614482,-0.577446189974434,2.26154741365496E-16));
#9169=CARTESIAN_POINT('Ctrl Pts',(2.47475215402615,-0.660408357948197,3.47506847049484E-16));
#9170=CARTESIAN_POINT('Ctrl Pts',(2.43933604293942,-0.741555503604727,2.77555756156289E-16));
#9171=CARTESIAN_POINT('Ctrl Pts',(2.40393876465244,-0.822659498618874,2.07641862313994E-16));
#9172=CARTESIAN_POINT('Ctrl Pts',(2.3644375894048,-0.901951185787608,-1.23823437954767E-16));
#9173=CARTESIAN_POINT('Ctrl Pts',(2.32100582430644,-0.979100944080977,-1.11022302462516E-16));
#9174=CARTESIAN_POINT('Ctrl Pts',(2.27823644108386,-1.05507408425856,-9.84163982743666E-17));
#9175=CARTESIAN_POINT('Ctrl Pts',(2.23165476456022,-1.1289707546069,2.53313632717541E-16));
#9176=CARTESIAN_POINT('Ctrl Pts',(2.18139506127574,-1.20043719637909,2.77555756156289E-16));
#9177=CARTESIAN_POINT('Ctrl Pts',(2.16608689289344,-1.2222045418435,2.84939454890925E-16));
#9178=CARTESIAN_POINT('Ctrl Pts',(2.15043733121093,-1.24374612322857,4.37114965090439E-17));
#9179=CARTESIAN_POINT('Ctrl Pts',(2.13444972694369,-1.26505107698559,0.));
#9180=CARTESIAN_POINT('Ctrl Pts',(2.12083931058568,-1.28318820912085,-3.72120586158607E-17));
#9181=CARTESIAN_POINT('Ctrl Pts',(2.10698390104784,-1.30115384375424,6.4814165885223E-17));
#9182=CARTESIAN_POINT('Ctrl Pts',(2.09288546869145,-1.31894102140198,5.55111512312578E-17));
#9183=CARTESIAN_POINT('Ctrl Pts',(2.08472665052523,-1.32923453095322,5.01274601200272E-17));
#9184=CARTESIAN_POINT('Ctrl Pts',(2.07648733901943,-1.33946704131009,1.07093663002969E-16));
#9185=CARTESIAN_POINT('Ctrl Pts',(2.06817568052718,-1.3496280615777,1.11022302462516E-16));
#9186=CARTESIAN_POINT('Ctrl Pts',(2.0141423836499,-1.41568388247163,1.36562011828508E-16));
#9187=CARTESIAN_POINT('Ctrl Pts',(1.95696807639868,-1.47883106712894,-2.06909962337776E-16));
#9188=CARTESIAN_POINT('Ctrl Pts',(1.89681447147471,-1.5387754276769,-2.22044604925031E-16));
#9189=CARTESIAN_POINT('Ctrl Pts',(1.83758356202805,-1.5978003023447,-2.36947097397864E-16));
#9190=CARTESIAN_POINT('Ctrl Pts',(1.77546340770889,-1.65372037608364,4.0590157288843E-16));
#9191=CARTESIAN_POINT('Ctrl Pts',(1.71058212140457,-1.70621256947127,4.44089209850063E-16));
#9192=CARTESIAN_POINT('Ctrl Pts',(1.64772546517897,-1.75706673624623,4.81085195985522E-16));
#9193=CARTESIAN_POINT('Ctrl Pts',(1.58227673616169,-1.80470390837557,2.58606592525932E-16));
#9194=CARTESIAN_POINT('Ctrl Pts',(1.5143365021986,-1.84878472647799,2.77555756156289E-16));
#9195=CARTESIAN_POINT('Ctrl Pts',(1.46963595841736,-1.87778722506477,2.90023153883192E-16));
#9196=CARTESIAN_POINT('Ctrl Pts',(1.42385657678108,-1.90524929950103,3.23574125955808E-17));
#9197=CARTESIAN_POINT('Ctrl Pts',(1.37702479013104,-1.93106208855763,5.55111512312578E-17));
#9198=CARTESIAN_POINT('Ctrl Pts',(0.261124777554701,2.92529416030267,11.058));
#9199=CARTESIAN_POINT('Ctrl Pts',(0.712806568001128,2.88599464153458,11.0335796606559));
#9200=CARTESIAN_POINT('Ctrl Pts',(1.15551467718148,2.74786827548953,11.0091593213117));
#9201=CARTESIAN_POINT('Ctrl Pts',(1.53904161881194,2.51335023952951,10.9847389819676));
#9202=CARTESIAN_POINT('Ctrl Pts',(2.36167356031087,2.01032944412425,10.9323594774631));
#9203=CARTESIAN_POINT('Ctrl Pts',(2.91203354584656,1.06384412118684,10.8799799729586));
#9204=CARTESIAN_POINT('Ctrl Pts',(2.94465829055491,0.100220893818898,10.8276004684541));
#9205=CARTESIAN_POINT('Ctrl Pts',(2.97728303526326,-0.863402333549067,10.7752209639496));
#9206=CARTESIAN_POINT('Ctrl Pts',(2.49217253914424,-1.84416346534755,10.7228414594451));
#9207=CARTESIAN_POINT('Ctrl Pts',(1.70632723287924,-2.40227529678238,10.6704619549406));
#9208=CARTESIAN_POINT('Ctrl Pts',(0.92048192661426,-2.96038712821718,10.6180824504361));
#9209=CARTESIAN_POINT('Ctrl Pts',(-0.166098189796688,-3.09584965928835,
10.5657029459315));
#9210=CARTESIAN_POINT('Ctrl Pts',(-1.0650088521454,-2.74748941090806,10.513323441427));
#9211=CARTESIAN_POINT('Ctrl Pts',(-1.96391951449414,-2.39912916252775,10.4609439369225));
#9212=CARTESIAN_POINT('Ctrl Pts',(-2.67516072278063,-1.56694613469595,10.408564432418));
#9213=CARTESIAN_POINT('Ctrl Pts',(-2.87955920487239,-0.624834891848815,
10.3561849279135));
#9214=CARTESIAN_POINT('Ctrl Pts',(-2.92379628688831,-0.420937818389941,
10.3448486576389));
#9215=CARTESIAN_POINT('Ctrl Pts',(-2.94429281596354,-0.211891698741057,
10.3335123873642));
#9216=CARTESIAN_POINT('Ctrl Pts',(-2.94242444587263,-0.00248500551853048,
10.3221761170896));
#9217=CARTESIAN_POINT('Origin',(0.,0.,-1.84858989190501));
#9218=CARTESIAN_POINT('',(-1.37702479013099,-1.93106208855767,0.));
#9219=CARTESIAN_POINT('Ctrl Pts',(-1.37989654081094,-1.93326688769301,3.07371315899641E-16));
#9220=CARTESIAN_POINT('Ctrl Pts',(-0.801986922861967,-2.34019513141193,
0.0475906520026623));
#9221=CARTESIAN_POINT('Ctrl Pts',(0.824868299691477,-2.62988338064349,0.147626409229032));
#9222=CARTESIAN_POINT('Ctrl Pts',(2.66596861578497,-0.838738147770652,0.30010727167911));
#9223=CARTESIAN_POINT('Ctrl Pts',(2.16631806184957,1.76615982799916,0.457442587350233));
#9224=CARTESIAN_POINT('Ctrl Pts',(-0.283824062622952,2.78024166545816,0.614777903021357));
#9225=CARTESIAN_POINT('Ctrl Pts',(-2.10236314538525,1.54689613835291,0.745160337872953));
#9226=CARTESIAN_POINT('Ctrl Pts',(-2.3682722008076,0.381486792202907,0.823097667500842));
#9227=CARTESIAN_POINT('Ctrl Pts',(-2.36802324146013,0.000186122305323062,
0.848589891905023));
#9228=CARTESIAN_POINT('Origin',(0.,0.,0.));
#9229=CARTESIAN_POINT('Ctrl Pts',(-1.03908919352509,2.13201587949044,-0.329233991005384));
#9230=CARTESIAN_POINT('Ctrl Pts',(-1.74163600084562,1.78961280339009,-0.276788885781676));
#9231=CARTESIAN_POINT('Ctrl Pts',(-2.77044124913769,0.362429281341372,-0.171898675334261));
#9232=CARTESIAN_POINT('Ctrl Pts',(-1.82442757362648,-2.1194917921021,-0.0145633596631371));
#9233=CARTESIAN_POINT('Ctrl Pts',(0.766254154833431,-2.68690713172521,0.142771956007986));
#9234=CARTESIAN_POINT('Ctrl Pts',(2.66596861578497,-0.838738147770652,0.30010727167911));
#9235=CARTESIAN_POINT('Ctrl Pts',(2.16631806184957,1.76615982799916,0.457442587350233));
#9236=CARTESIAN_POINT('Ctrl Pts',(-0.283824062622952,2.78024166545816,0.614777903021357));
#9237=CARTESIAN_POINT('Ctrl Pts',(-2.47829466728951,1.29193683314281,0.772113218692479));
#9238=CARTESIAN_POINT('Ctrl Pts',(-2.44182858239548,-1.35964121596809,0.929448534363604));
#9239=CARTESIAN_POINT('Ctrl Pts',(-0.207121339063888,-2.78711087979173,
1.08678385003473));
#9240=CARTESIAN_POINT('Ctrl Pts',(2.21401803077907,-1.70561830406782,1.24411916570585));
#9241=CARTESIAN_POINT('Ctrl Pts',(2.64205485235054,0.911349150745493,1.40145448137697));
#9242=CARTESIAN_POINT('Ctrl Pts',(0.691640660298454,2.70787919402874,1.5587897970481));
#9243=CARTESIAN_POINT('Ctrl Pts',(-1.88140253096646,2.06671733364312,1.71612511271922));
#9244=CARTESIAN_POINT('Ctrl Pts',(-2.76076141176456,-0.43496057134077,1.87346042839035));
#9245=CARTESIAN_POINT('Ctrl Pts',(-1.15481219883121,-2.54507342378116,2.03079574406147));
#9246=CARTESIAN_POINT('Ctrl Pts',(1.49072764255621,-2.36404822464922,2.18813105973259));
#9247=CARTESIAN_POINT('Ctrl Pts',(2.79427705549031,-0.0548463935276453,
2.34546637540372));
#9248=CARTESIAN_POINT('Ctrl Pts',(1.5823475414007,2.30372918060613,2.50280169107483));
#9249=CARTESIAN_POINT('Ctrl Pts',(-1.05405113312049,2.58842974112365,2.66013700674597));
#9250=CARTESIAN_POINT('Ctrl Pts',(-2.74156638658485,0.542960359863138,2.81747232241708));
#9251=CARTESIAN_POINT('Ctrl Pts',(-1.9610543025963,-1.99129560121778,2.97480763808821));
#9252=CARTESIAN_POINT('Ctrl Pts',(0.584848394656438,-2.73293698550247,3.13214295375933));
#9253=CARTESIAN_POINT('Ctrl Pts',(2.60425579784155,-1.01431944186932,3.28947826943046));
#9254=CARTESIAN_POINT('Ctrl Pts',(2.27924634057658,1.61741407950708,3.44681358510158));
#9255=CARTESIAN_POINT('Ctrl Pts',(-0.0975982492034651,2.79311059143494,
3.6041489007727));
#9256=CARTESIAN_POINT('Ctrl Pts',(-2.38658243027454,1.45437838755459,3.76148421644382));
#9257=CARTESIAN_POINT('Ctrl Pts',(-2.52710481755741,-1.19362198012869,3.91881953211495));
#9258=CARTESIAN_POINT('Ctrl Pts',(-0.392663608746353,-2.76709368867159,
4.07615484778607));
#9259=CARTESIAN_POINT('Ctrl Pts',(2.09526330020315,-1.8495577562663,4.23349016345719));
#9260=CARTESIAN_POINT('Ctrl Pts',(2.69698125586998,0.732996791565816,4.39082547912832));
#9261=CARTESIAN_POINT('Ctrl Pts',(0.870808554093777,2.65568911080063,4.54816079479944));
#9262=CARTESIAN_POINT('Ctrl Pts',(-1.73928800639316,2.18766300463189,4.70549611047057));
#9263=CARTESIAN_POINT('Ctrl Pts',(-2.78363356575401,-0.249752602863106,
4.86283142614169));
#9264=CARTESIAN_POINT('Ctrl Pts',(-1.32208186928512,-2.46233460804071,5.02016674181281));
#9265=CARTESIAN_POINT('Ctrl Pts',(1.32964132424929,-2.45826079574207,5.17750205748394));
#9266=CARTESIAN_POINT('Ctrl Pts',(2.78438780839412,-0.241198514719961,5.33483737315506));
#9267=CARTESIAN_POINT('Ctrl Pts',(1.73255804842731,2.19299676239354,5.49217268882618));
#9268=CARTESIAN_POINT('Ctrl Pts',(-0.878964234485193,2.65300095467984,5.64950800449731));
#9269=CARTESIAN_POINT('Ctrl Pts',(-2.69922070918587,0.72470666765315,5.80684332016843));
#9270=CARTESIAN_POINT('Ctrl Pts',(-2.08957051396587,-1.85598686908106,5.96417863583956));
#9271=CARTESIAN_POINT('Ctrl Pts',(0.401163844498212,-2.76587414046649,6.12151395151068));
#9272=CARTESIAN_POINT('Ctrl Pts',(2.53076037597685,-1.18585163930103,6.2788492671818));
#9273=CARTESIAN_POINT('Ctrl Pts',(2.38210248511723,1.46170446446183,6.43618458285292));
#9274=CARTESIAN_POINT('Ctrl Pts',(0.0890157606711408,2.793397283841,6.59351989852405));
#9275=CARTESIAN_POINT('Ctrl Pts',(-2.28420520026003,1.61040330172691,6.75085521419516));
#9276=CARTESIAN_POINT('Ctrl Pts',(-2.60112693645964,-1.02231641451357,6.9081905298663));
#9277=CARTESIAN_POINT('Ctrl Pts',(-0.57644849505612,-2.73472106868152,7.06552584553741));
#9278=CARTESIAN_POINT('Ctrl Pts',(1.96716344393165,-1.98526073259378,7.22286116120855));
#9279=CARTESIAN_POINT('Ctrl Pts',(2.73988515609665,0.551381466653972,7.38019647687966));
#9280=CARTESIAN_POINT('Ctrl Pts',(1.04609303646807,2.5916561403346,7.53753179255079));
#9281=CARTESIAN_POINT('Ctrl Pts',(-1.58941846186445,2.2988564868904,7.69486710822191));
#9282=CARTESIAN_POINT('Ctrl Pts',(-2.79409530723714,-0.0634318507917163,
7.85220242389303));
#9283=CARTESIAN_POINT('Ctrl Pts',(-1.48345697628832,-2.36861723168749,8.00953773956416));
#9284=CARTESIAN_POINT('Ctrl Pts',(1.16262680634646,-2.54151354917186,8.16687305523529));
#9285=CARTESIAN_POINT('Ctrl Pts',(2.76208455499713,-0.426475157784177,8.3242083709064));
#9286=CARTESIAN_POINT('Ctrl Pts',(1.8750440359881,2.07248692819523,8.48154368657753));
#9287=CARTESIAN_POINT('Ctrl Pts',(-0.699958537943023,2.7057439570526,8.63887900224866));
#9288=CARTESIAN_POINT('Ctrl Pts',(-2.6448406647993,0.903221864868725,8.79621431791976));
#9289=CARTESIAN_POINT('Ctrl Pts',(-2.20877058145475,-1.7124032551425,8.95354963359091));
#9290=CARTESIAN_POINT('Ctrl Pts',(0.215690902196592,-2.78647992051942,9.11088494926201));
#9291=CARTESIAN_POINT('Ctrl Pts',(2.4459813653409,-1.35209655994371,9.26822026493315));
#9292=CARTESIAN_POINT('Ctrl Pts',(2.47433880171217,1.29947749716991,9.42555558060427));
#9293=CARTESIAN_POINT('Ctrl Pts',(0.275231669725872,2.78123058171878,9.58289089627539));
#9294=CARTESIAN_POINT('Ctrl Pts',(-2.17164161907558,1.7592467736877,9.74022621194653));
#9295=CARTESIAN_POINT('Ctrl Pts',(-2.66355657074516,-0.846449946443288,
9.89756152761763));
#9296=CARTESIAN_POINT('Ctrl Pts',(-0.757654725048104,-2.69016151139635,
10.0548968432888));
#9297=CARTESIAN_POINT('Ctrl Pts',(1.83027666927001,-2.11210170665972,10.2122321589599));
#9298=CARTESIAN_POINT('Ctrl Pts',(2.77060484795253,0.367287133540841,10.369567474631));
#9299=CARTESIAN_POINT('Ctrl Pts',(1.21665350181368,2.51610800548609,10.5269027903021));
#9300=CARTESIAN_POINT('Ctrl Pts',(-1.43234772356642,2.39972494583597,10.6842381059733));
#9301=CARTESIAN_POINT('Ctrl Pts',(-2.79231938150401,0.123316482315984,10.8415734216444));
#9302=CARTESIAN_POINT('Ctrl Pts',(-1.63779792657952,-2.26461658842463,10.9989087373155));
#9303=CARTESIAN_POINT('Ctrl Pts',(0.989622905930635,-2.61290295808564,11.1562440529866));
#9304=CARTESIAN_POINT('Ctrl Pts',(2.72902843688469,-0.61088887604173,11.3135793686578));
#9305=CARTESIAN_POINT('Ctrl Pts',(2.00599839187704,1.9449087769569,11.4709146843289));
#9306=CARTESIAN_POINT('Ctrl Pts',(0.328567026486064,2.47549058867235,11.5758048947763));
#9307=CARTESIAN_POINT('Ctrl Pts',(-0.439445221994061,2.3306835819919,11.62825));
#9308=CARTESIAN_POINT('Ctrl Pts',(-1.12236674703447,2.30288577939268,-0.219489327336923));
#9309=CARTESIAN_POINT('Ctrl Pts',(-1.881218999262,1.93304089110777,-0.167044222113215));
#9310=CARTESIAN_POINT('Ctrl Pts',(-2.9924775967461,0.391476088928602,-0.0621540116657994));
#9311=CARTESIAN_POINT('Ctrl Pts',(-1.97064588273166,-2.28935795203269,0.0951813040053245));
#9312=CARTESIAN_POINT('Ctrl Pts',(0.82766540978493,-2.90224865758394,0.252516619676447));
#9313=CARTESIAN_POINT('Ctrl Pts',(2.87963202931947,-0.905958614903406,0.409851935347572));
#9314=CARTESIAN_POINT('Ctrl Pts',(2.33993710190716,1.90770828264466,0.567187251018694));
#9315=CARTESIAN_POINT('Ctrl Pts',(-0.306571073860874,3.00306346507554,0.724522566689817));
#9316=CARTESIAN_POINT('Ctrl Pts',(-2.67691699735827,1.39547879991837,0.881857882360941));
#9317=CARTESIAN_POINT('Ctrl Pts',(-2.63752834686069,-1.46860933422193,1.03919319803207));
#9318=CARTESIAN_POINT('Ctrl Pts',(-0.223721028969555,-3.01048321093979,
1.19652851370319));
#9319=CARTESIAN_POINT('Ctrl Pts',(2.39145997337443,-1.84231467283839,1.35386382937431));
#9320=CARTESIAN_POINT('Ctrl Pts',(2.85380170306596,0.984389009248359,1.51119914504543));
#9321=CARTESIAN_POINT('Ctrl Pts',(0.747072034675363,2.92490152077689,1.66853446071656));
#9322=CARTESIAN_POINT('Ctrl Pts',(-2.03218708432488,2.23235389729304,1.82586977638768));
#9323=CARTESIAN_POINT('Ctrl Pts',(-2.98202197113476,-0.469820381720866,
1.98320509205881));
#9324=CARTESIAN_POINT('Ctrl Pts',(-1.24736434476896,-2.74904772122835,2.14054040772993));
#9325=CARTESIAN_POINT('Ctrl Pts',(1.61020165094208,-2.55351430104939,2.29787572340105));
#9326=CARTESIAN_POINT('Ctrl Pts',(3.01822371806624,-0.0592420445461263,
2.45521103907218));
#9327=CARTESIAN_POINT('Ctrl Pts',(1.70916440454448,2.48836100172844,2.6125463547433));
#9328=CARTESIAN_POINT('Ctrl Pts',(-1.13852780768032,2.79587882019688,2.76988167041443));
#9329=CARTESIAN_POINT('Ctrl Pts',(-2.9612885652785,0.586475787319947,2.92721698608554));
#9330=CARTESIAN_POINT('Ctrl Pts',(-2.11822252803541,-2.15088750826171,3.08455230175667));
#9331=CARTESIAN_POINT('Ctrl Pts',(0.631720928587459,-2.95196756292179,3.24188761742779));
#9332=CARTESIAN_POINT('Ctrl Pts',(2.81297325242419,-1.09561182958951,3.39922293309892));
#9333=CARTESIAN_POINT('Ctrl Pts',(2.46191599037299,1.74704134191371,3.55655824877004));
#9334=CARTESIAN_POINT('Ctrl Pts',(-0.105420237413036,3.01696376802969,3.71389356444116));
#9335=CARTESIAN_POINT('Ctrl Pts',(-2.57785450516496,1.57093919364055,3.87122888011228));
#9336=CARTESIAN_POINT('Ctrl Pts',(-2.72963902538035,-1.28928452665457,4.02856419578341));
#9337=CARTESIAN_POINT('Ctrl Pts',(-0.424133539231963,-2.98886174685155,
4.18589951145453));
#9338=CARTESIAN_POINT('Ctrl Pts',(2.26318767347756,-1.99779011781522,4.34323482712566));
#9339=CARTESIAN_POINT('Ctrl Pts',(2.91313016998542,0.791742643136777,4.50057014279678));
#9340=CARTESIAN_POINT('Ctrl Pts',(0.940599296228219,2.86852867588043,4.6579054584679));
#9341=CARTESIAN_POINT('Ctrl Pts',(-1.87868282535885,2.36299272999521,4.81524077413902));
#9342=CARTESIAN_POINT('Ctrl Pts',(-3.00672720840483,-0.269768965152914,
4.97257608981016));
#9343=CARTESIAN_POINT('Ctrl Pts',(-1.42803980273229,-2.65967782299944,5.12991140548127));
#9344=CARTESIAN_POINT('Ctrl Pts',(1.43620510839645,-2.65527751599392,5.28724672115241));
#9345=CARTESIAN_POINT('Ctrl Pts',(3.00754189963992,-0.260529311672868,5.44458203682351));
#9346=CARTESIAN_POINT('Ctrl Pts',(1.87141349653044,2.36875396048986,5.60191735249465));
#9347=CARTESIAN_POINT('Ctrl Pts',(-0.949408611663097,2.86562507813386,5.75925266816576));
#9348=CARTESIAN_POINT('Ctrl Pts',(-2.9155491037487,0.782788109236974,5.9165879838369));
#9349=CARTESIAN_POINT('Ctrl Pts',(-2.25703864025646,-2.00473449033026,6.07392329950801));
#9350=CARTESIAN_POINT('Ctrl Pts',(0.433315024333776,-2.98754445824887,6.23125861517914));
#9351=CARTESIAN_POINT('Ctrl Pts',(2.73358755765012,-1.28089143373012,6.38859393085026));
#9352=CARTESIAN_POINT('Ctrl Pts',(2.57301551588047,1.57885241721953,6.54592924652138));
#9353=CARTESIAN_POINT('Ctrl Pts',(0.0961499074014511,3.01727343732968,6.70326456219251));
#9354=CARTESIAN_POINT('Ctrl Pts',(-2.46727227667312,1.73946868703451,6.86059987786364));
#9355=CARTESIAN_POINT('Ctrl Pts',(-2.80959362919934,-1.104249717683,7.01793519353475));
#9356=CARTESIAN_POINT('Ctrl Pts',(-0.622647821053927,-2.95389463101813,
7.17527050920589));
#9357=CARTESIAN_POINT('Ctrl Pts',(2.12482128503379,-2.14436897654329,7.33260582487699));
#9358=CARTESIAN_POINT('Ctrl Pts',(2.95947259297716,0.59557180168919,7.48994114054813));
#9359=CARTESIAN_POINT('Ctrl Pts',(1.12993191128569,2.79936379839662,7.64727645621924));
#9360=CARTESIAN_POINT('Ctrl Pts',(-1.71680202222819,2.4830977871468,7.80461177189038));
#9361=CARTESIAN_POINT('Ctrl Pts',(-3.01802740364303,-0.0685155812177535,
7.96194708756148));
#9362=CARTESIAN_POINT('Ctrl Pts',(-1.60234827887482,-2.55844949005786,8.11928240323263));
#9363=CARTESIAN_POINT('Ctrl Pts',(1.25580525212405,-2.74520254132467,8.27661771890373));
#9364=CARTESIAN_POINT('Ctrl Pts',(2.98345115736347,-0.460654906735591,8.43395303457487));
#9365=CARTESIAN_POINT('Ctrl Pts',(2.02531898929576,2.23858589461288,8.591288350246));
#9366=CARTESIAN_POINT('Ctrl Pts',(-0.756056546623237,2.92259515574686,8.74862366591711));
#9367=CARTESIAN_POINT('Ctrl Pts',(-2.85681078378342,0.975610363999675,8.90595898158824));
#9368=CARTESIAN_POINT('Ctrl Pts',(-2.38579196848608,-1.84964340218511,9.06329429725935));
#9369=CARTESIAN_POINT('Ctrl Pts',(0.232977397678477,-3.00980168358836,9.2206296129305));
#9370=CARTESIAN_POINT('Ctrl Pts',(2.6420139535965,-1.46046001355504,9.37796492860159));
#9371=CARTESIAN_POINT('Ctrl Pts',(2.67264408988566,1.40362380865033,9.53530024427275));
#9372=CARTESIAN_POINT('Ctrl Pts',(0.297290045701602,3.00413163779202,9.69263555994384));
#9373=CARTESIAN_POINT('Ctrl Pts',(-2.34568731434669,1.90024118325806,9.84997087561499));
#9374=CARTESIAN_POINT('Ctrl Pts',(-2.87702667151006,-0.914288473825907,
10.0073061912861));
#9375=CARTESIAN_POINT('Ctrl Pts',(-0.818376780767691,-2.90576385873112,
10.1646415069572));
#9376=CARTESIAN_POINT('Ctrl Pts',(1.97696375273877,-2.2813755899699,10.3219768226283));
#9377=CARTESIAN_POINT('Ctrl Pts',(2.99265430714862,0.396723272524227,10.4793121382995));
#9378=CARTESIAN_POINT('Ctrl Pts',(1.31416190410585,2.71776087645035,10.6366474539706));
#9379=CARTESIAN_POINT('Ctrl Pts',(-1.54714288738549,2.59205032447523,10.7939827696417));
#9380=CARTESIAN_POINT('Ctrl Pts',(-3.01610914676913,0.133199652133039,10.9513180853128));
#9381=CARTESIAN_POINT('Ctrl Pts',(-1.76905884750739,-2.44611374025332,11.108653400984));
#9382=CARTESIAN_POINT('Ctrl Pts',(1.06893599571762,-2.82231343724637,11.2659887166551));
#9383=CARTESIAN_POINT('Ctrl Pts',(2.94774576461505,-0.659848418090555,11.4233240323262));
#9384=CARTESIAN_POINT('Ctrl Pts',(2.1667686505423,2.10078302312668,11.5806593479973));
#9385=CARTESIAN_POINT('Ctrl Pts',(0.35489995180194,2.67388818653474,11.6855495584447));
#9386=CARTESIAN_POINT('Ctrl Pts',(-0.474664453622185,2.51747565713064,11.7379946636685));
#9387=CARTESIAN_POINT('Ctrl Pts',(-1.20564430054384,2.47375567929493,-0.109744663668461));
#9388=CARTESIAN_POINT('Ctrl Pts',(-2.02080199767838,2.07646897882546,-0.0572995584447534));
#9389=CARTESIAN_POINT('Ctrl Pts',(-3.21451394435451,0.420522896515832,0.0475906520026618));
#9390=CARTESIAN_POINT('Ctrl Pts',(-2.11686419183683,-2.45922411196328,0.204925967673786));
#9391=CARTESIAN_POINT('Ctrl Pts',(0.88907666473643,-3.11759018344267,0.362261283344908));
#9392=CARTESIAN_POINT('Ctrl Pts',(3.09329544285396,-0.973179082036162,0.519596599016033));
#9393=CARTESIAN_POINT('Ctrl Pts',(2.51355614196476,2.04925673729017,0.676931914687155));
#9394=CARTESIAN_POINT('Ctrl Pts',(-0.329318085098797,3.22588526469291,0.83426723035828));
#9395=CARTESIAN_POINT('Ctrl Pts',(-2.87553932742704,1.49902076669393,0.991602546029402));
#9396=CARTESIAN_POINT('Ctrl Pts',(-2.8332281113259,-1.57757745247578,1.14893786170053));
#9397=CARTESIAN_POINT('Ctrl Pts',(-0.240320718875223,-3.23385554208785,
1.30627317737165));
#9398=CARTESIAN_POINT('Ctrl Pts',(2.5689019159698,-1.97901104160895,1.46360849304277));
#9399=CARTESIAN_POINT('Ctrl Pts',(3.06554855378139,1.05742886775122,1.6209438087139));
#9400=CARTESIAN_POINT('Ctrl Pts',(0.802503409052275,3.14192384752506,1.77827912438502));
#9401=CARTESIAN_POINT('Ctrl Pts',(-2.18297163768331,2.39799046094296,1.93561444005614));
#9402=CARTESIAN_POINT('Ctrl Pts',(-3.20328253050495,-0.504680192100957,
2.09294975572727));
#9403=CARTESIAN_POINT('Ctrl Pts',(-1.33991649070671,-2.95302201867555,2.25028507139839));
#9404=CARTESIAN_POINT('Ctrl Pts',(1.72967565932795,-2.74298037744955,2.40762038706951));
#9405=CARTESIAN_POINT('Ctrl Pts',(3.24217038064216,-0.0636376955646108,
2.56495570274064));
#9406=CARTESIAN_POINT('Ctrl Pts',(1.83598126768827,2.67299282285076,2.72229101841176));
#9407=CARTESIAN_POINT('Ctrl Pts',(-1.22300448224015,3.00332789927011,2.87962633408289));
#9408=CARTESIAN_POINT('Ctrl Pts',(-3.18101074397215,0.629991214776759,3.036961649754));
#9409=CARTESIAN_POINT('Ctrl Pts',(-2.27539075347452,-2.31047941530565,3.19429696542514));
#9410=CARTESIAN_POINT('Ctrl Pts',(0.678593462518484,-3.1709981403411,3.35163228109625));
#9411=CARTESIAN_POINT('Ctrl Pts',(3.02169070700682,-1.1769042173097,3.50896759676738));
#9412=CARTESIAN_POINT('Ctrl Pts',(2.64458564016939,1.87666860432035,3.6663029124385));
#9413=CARTESIAN_POINT('Ctrl Pts',(-0.113242225622608,3.24081694462443,3.82363822810962));
#9414=CARTESIAN_POINT('Ctrl Pts',(-2.76912658005537,1.68749999972651,3.98097354378075));
#9415=CARTESIAN_POINT('Ctrl Pts',(-2.93217323320329,-1.38494707318046,4.13830885945187));
#9416=CARTESIAN_POINT('Ctrl Pts',(-0.45560346971757,-3.21062980503151,4.295644175123));
#9417=CARTESIAN_POINT('Ctrl Pts',(2.43111204675198,-2.14602247936414,4.45297949079412));
#9418=CARTESIAN_POINT('Ctrl Pts',(3.12927908410086,0.850488494707743,4.61031480646524));
#9419=CARTESIAN_POINT('Ctrl Pts',(1.01039003836266,3.08136824096022,4.76765012213636));
#9420=CARTESIAN_POINT('Ctrl Pts',(-2.01807764432454,2.53832245535854,4.92498543780749));
#9421=CARTESIAN_POINT('Ctrl Pts',(-3.22982085105565,-0.289785327442726,
5.08232075347861));
#9422=CARTESIAN_POINT('Ctrl Pts',(-1.53399773617946,-2.85702103795818,5.23965606914974));
#9423=CARTESIAN_POINT('Ctrl Pts',(1.5427688925436,-2.85229423624577,5.39699138482085));
#9424=CARTESIAN_POINT('Ctrl Pts',(3.23069599088573,-0.279860108625777,5.55432670049199));
#9425=CARTESIAN_POINT('Ctrl Pts',(2.01026894463356,2.54451115858618,5.7116620161631));
#9426=CARTESIAN_POINT('Ctrl Pts',(-1.019852988841,3.07824920158788,5.86899733183423));
#9427=CARTESIAN_POINT('Ctrl Pts',(-3.13187749831153,0.840869550820803,6.02633264750535));
#9428=CARTESIAN_POINT('Ctrl Pts',(-2.42450676654705,-2.15348211157947,6.18366796317648));
#9429=CARTESIAN_POINT('Ctrl Pts',(0.465466204169338,-3.20921477603124,6.3410032788476));
#9430=CARTESIAN_POINT('Ctrl Pts',(2.93641473932339,-1.3759312281592,6.49833859451872));
#9431=CARTESIAN_POINT('Ctrl Pts',(2.76392854664371,1.69600036997724,6.65567391018985));
#9432=CARTESIAN_POINT('Ctrl Pts',(0.103284054131762,3.24114959081836,6.81300922586097));
#9433=CARTESIAN_POINT('Ctrl Pts',(-2.65033935308621,1.86853407234211,6.97034454153209));
#9434=CARTESIAN_POINT('Ctrl Pts',(-3.01806032193904,-1.18618302085242,7.12767985720322));
#9435=CARTESIAN_POINT('Ctrl Pts',(-0.668847147051728,-3.17306819335475,
7.28501517287434));
#9436=CARTESIAN_POINT('Ctrl Pts',(2.28247912613591,-2.30347722049279,7.44235048854546));
#9437=CARTESIAN_POINT('Ctrl Pts',(3.17906002985769,0.639762136724403,7.59968580421659));
#9438=CARTESIAN_POINT('Ctrl Pts',(1.2137707861033,3.00707145645863,7.75702111988771));
#9439=CARTESIAN_POINT('Ctrl Pts',(-1.84418558259193,2.66733908740319,7.91435643555884));
#9440=CARTESIAN_POINT('Ctrl Pts',(-3.24195950004891,-0.0735993116437874,
8.07169175122995));
#9441=CARTESIAN_POINT('Ctrl Pts',(-1.7212395814613,-2.74828174842822,8.22902706690109));
#9442=CARTESIAN_POINT('Ctrl Pts',(1.34898369790163,-2.94889153347749,8.38636238257219));
#9443=CARTESIAN_POINT('Ctrl Pts',(3.20481775972981,-0.494834655687006,8.54369769824334));
#9444=CARTESIAN_POINT('Ctrl Pts',(2.17559394260342,2.40468486103055,8.70103301391445));
#9445=CARTESIAN_POINT('Ctrl Pts',(-0.812154555303452,3.13944635444111,8.85836832958556));
#9446=CARTESIAN_POINT('Ctrl Pts',(-3.06878090276754,1.04799886313063,9.01570364525671));
#9447=CARTESIAN_POINT('Ctrl Pts',(-2.56281335551741,-1.98688354922771,9.17303896092782));
#9448=CARTESIAN_POINT('Ctrl Pts',(0.250263893160364,-3.23312344665729,9.33037427659894));
#9449=CARTESIAN_POINT('Ctrl Pts',(2.83804654185209,-1.56882346716636,9.48770959227006));
#9450=CARTESIAN_POINT('Ctrl Pts',(2.87094937805915,1.50777012013074,9.64504490794121));
#9451=CARTESIAN_POINT('Ctrl Pts',(0.31934842167733,3.22703269386527,9.8023802236123));
#9452=CARTESIAN_POINT('Ctrl Pts',(-2.5197330096178,2.04123559282842,9.95971553928346));
#9453=CARTESIAN_POINT('Ctrl Pts',(-3.09049677227496,-0.982127001208522,
10.1170508549545));
#9454=CARTESIAN_POINT('Ctrl Pts',(-0.879098836487281,-3.1213662060659,10.2743861706257));
#9455=CARTESIAN_POINT('Ctrl Pts',(2.12365083620754,-2.45064947328008,10.4317214862968));
#9456=CARTESIAN_POINT('Ctrl Pts',(3.2147037663447,0.426159411507612,10.5890568019679));
#9457=CARTESIAN_POINT('Ctrl Pts',(1.41167030639802,2.9194137474146,10.7463921176391));
#9458=CARTESIAN_POINT('Ctrl Pts',(-1.66193805120456,2.78437570311449,10.9037274333102));
#9459=CARTESIAN_POINT('Ctrl Pts',(-3.23989891203425,0.143082821950096,11.0610627489813));
#9460=CARTESIAN_POINT('Ctrl Pts',(-1.90031976843527,-2.627610892082,11.2183980646524));
#9461=CARTESIAN_POINT('Ctrl Pts',(1.1482490855046,-3.0317239164071,11.3757333803236));
#9462=CARTESIAN_POINT('Ctrl Pts',(3.16646309234541,-0.708807960139384,11.5330686959947));
#9463=CARTESIAN_POINT('Ctrl Pts',(2.32753890920755,2.25665726929647,11.6904040116658));
#9464=CARTESIAN_POINT('Ctrl Pts',(0.381232877117816,2.87228578439713,11.7952942221132));
#9465=CARTESIAN_POINT('Ctrl Pts',(-0.50988368525031,2.70426773226937,11.8477393273369));
#9466=CARTESIAN_POINT('Ctrl Pts',(-1.28892185405322,2.64462557919718,0.));
#9467=CARTESIAN_POINT('Ctrl Pts',(-2.16038499609476,2.21989706654315,0.0524451052237078));
#9468=CARTESIAN_POINT('Ctrl Pts',(-3.43655029196293,0.449569704103062,0.157335315671123));
#9469=CARTESIAN_POINT('Ctrl Pts',(-2.26308250094201,-2.62909027189387,0.314670631342247));
#9470=CARTESIAN_POINT('Ctrl Pts',(0.950487919687924,-3.33293170930141,0.47200594701337));
#9471=CARTESIAN_POINT('Ctrl Pts',(3.30695885638846,-1.04039954916892,0.629341262684495));
#9472=CARTESIAN_POINT('Ctrl Pts',(2.68717518202235,2.19080519193567,0.786676578355616));
#9473=CARTESIAN_POINT('Ctrl Pts',(-0.352065096336719,3.44870706431028,0.944011894026741));
#9474=CARTESIAN_POINT('Ctrl Pts',(-3.0741616574958,1.60256273346949,1.10134720969786));
#9475=CARTESIAN_POINT('Ctrl Pts',(-3.02892787579111,-1.68654557072963,1.25868252536899));
#9476=CARTESIAN_POINT('Ctrl Pts',(-0.256920408780888,-3.45722787323591,
1.41601784104011));
#9477=CARTESIAN_POINT('Ctrl Pts',(2.74634385856517,-2.11570741037952,1.57335315671124));
#9478=CARTESIAN_POINT('Ctrl Pts',(3.27729540449682,1.13046872625408,1.73068847238236));
#9479=CARTESIAN_POINT('Ctrl Pts',(0.857934783429182,3.35894617427322,1.88802378805348));
#9480=CARTESIAN_POINT('Ctrl Pts',(-2.33375619104173,2.56362702459287,2.0453591037246));
#9481=CARTESIAN_POINT('Ctrl Pts',(-3.42454308987515,-0.539540002481048,
2.20269441939573));
#9482=CARTESIAN_POINT('Ctrl Pts',(-1.43246863664446,-3.15699631612275,2.36002973506685));
#9483=CARTESIAN_POINT('Ctrl Pts',(1.84914966771382,-2.93244645384971,2.51736505073797));
#9484=CARTESIAN_POINT('Ctrl Pts',(3.46611704321809,-0.0680333465830936,
2.6747003664091));
#9485=CARTESIAN_POINT('Ctrl Pts',(1.96279813083206,2.85762464397308,2.83203568208022));
#9486=CARTESIAN_POINT('Ctrl Pts',(-1.30748115679998,3.21077697834334,2.98937099775135));
#9487=CARTESIAN_POINT('Ctrl Pts',(-3.40073292266579,0.673506642233569,3.14670631342246));
#9488=CARTESIAN_POINT('Ctrl Pts',(-2.43255897891363,-2.47007132234958,3.3040416290936));
#9489=CARTESIAN_POINT('Ctrl Pts',(0.725465996449509,-3.39002871776042,3.46137694476471));
#9490=CARTESIAN_POINT('Ctrl Pts',(3.23040816158946,-1.2581966050299,3.61871226043584));
#9491=CARTESIAN_POINT('Ctrl Pts',(2.8272552899658,2.00629586672699,3.77604757610696));
#9492=CARTESIAN_POINT('Ctrl Pts',(-0.12106421383218,3.46467012121918,3.93338289177809));
#9493=CARTESIAN_POINT('Ctrl Pts',(-2.96039865494578,1.80406080581246,4.09071820744921));
#9494=CARTESIAN_POINT('Ctrl Pts',(-3.13470744102623,-1.48060961970634,4.24805352312033));
#9495=CARTESIAN_POINT('Ctrl Pts',(-0.48707340020318,-3.43239786321147,4.40538883879146));
#9496=CARTESIAN_POINT('Ctrl Pts',(2.59903642002639,-2.29425484091306,4.56272415446258));
#9497=CARTESIAN_POINT('Ctrl Pts',(3.3454279982163,0.909234346278705,4.7200594701337));
#9498=CARTESIAN_POINT('Ctrl Pts',(1.0801807804971,3.29420780604002,4.87739478580482));
#9499=CARTESIAN_POINT('Ctrl Pts',(-2.15747246329023,2.71365218072187,5.03473010147595));
#9500=CARTESIAN_POINT('Ctrl Pts',(-3.45291449370647,-0.309801689732533,
5.19206541714708));
#9501=CARTESIAN_POINT('Ctrl Pts',(-1.63995566962662,-3.05436425291692,5.34940073281819));
#9502=CARTESIAN_POINT('Ctrl Pts',(1.64933267669075,-3.04931095649762,5.50673604848933));
#9503=CARTESIAN_POINT('Ctrl Pts',(3.45385008213154,-0.299190905578683,5.66407136416044));
#9504=CARTESIAN_POINT('Ctrl Pts',(2.14912439273668,2.7202683566825,5.82140667983157));
#9505=CARTESIAN_POINT('Ctrl Pts',(-1.0902973660189,3.2908733250419,5.97874199550268));
#9506=CARTESIAN_POINT('Ctrl Pts',(-3.34820589287437,0.898950992404627,6.13607731117382));
#9507=CARTESIAN_POINT('Ctrl Pts',(-2.59197489283764,-2.30222973282867,6.29341262684493));
#9508=CARTESIAN_POINT('Ctrl Pts',(0.497617384004899,-3.43088509381362,6.45074794251607));
#9509=CARTESIAN_POINT('Ctrl Pts',(3.13924192099666,-1.47097102258828,6.60808325818718));
#9510=CARTESIAN_POINT('Ctrl Pts',(2.95484157740695,1.81314832273494,6.76541857385831));
#9511=CARTESIAN_POINT('Ctrl Pts',(0.110418200862072,3.46502574430704,6.92275388952943));
#9512=CARTESIAN_POINT('Ctrl Pts',(-2.8334064294993,1.9975994576497,7.08008920520056));
#9513=CARTESIAN_POINT('Ctrl Pts',(-3.22652701467874,-1.26811632402185,7.23742452087168));
#9514=CARTESIAN_POINT('Ctrl Pts',(-0.715046473049532,-3.39224175569136,
7.3947598365428));
#9515=CARTESIAN_POINT('Ctrl Pts',(2.44013696723805,-2.46258546444229,7.55209515221393));
#9516=CARTESIAN_POINT('Ctrl Pts',(3.39864746673821,0.683952471759619,7.70943046788505));
#9517=CARTESIAN_POINT('Ctrl Pts',(1.29760966092091,3.21477911452065,7.86676578355617));
#9518=CARTESIAN_POINT('Ctrl Pts',(-1.97156914295567,2.85158038765959,8.0241010992273));
#9519=CARTESIAN_POINT('Ctrl Pts',(-3.4658915964548,-0.0786830420698247,
8.18143641489842));
#9520=CARTESIAN_POINT('Ctrl Pts',(-1.84013088404779,-2.93811400679859,8.33877173056954));
#9521=CARTESIAN_POINT('Ctrl Pts',(1.44216214367922,-3.1525805256303,8.49610704624066));
#9522=CARTESIAN_POINT('Ctrl Pts',(3.42618436209615,-0.529014404638419,8.6534423619118));
#9523=CARTESIAN_POINT('Ctrl Pts',(2.32586889591107,2.57078382744821,8.81077767758291));
#9524=CARTESIAN_POINT('Ctrl Pts',(-0.868252563983666,3.35629755313536,8.96811299325404));
#9525=CARTESIAN_POINT('Ctrl Pts',(-3.28075102175166,1.12038736226158,9.12544830892515));
#9526=CARTESIAN_POINT('Ctrl Pts',(-2.73983474254873,-2.12412369627032,9.28278362459629));
#9527=CARTESIAN_POINT('Ctrl Pts',(0.267550388642249,-3.45644520972622,9.44011894026741));
#9528=CARTESIAN_POINT('Ctrl Pts',(3.03407913010768,-1.67718692077769,9.59745425593853));
#9529=CARTESIAN_POINT('Ctrl Pts',(3.06925466623264,1.61191643161116,9.75478957160966));
#9530=CARTESIAN_POINT('Ctrl Pts',(0.341406797653059,3.4499337499385,9.91212488728077));
#9531=CARTESIAN_POINT('Ctrl Pts',(-2.69377870488891,2.18223000239878,10.0694602029519));
#9532=CARTESIAN_POINT('Ctrl Pts',(-3.30396687303986,-1.04996552859114,10.226795518623));
#9533=CARTESIAN_POINT('Ctrl Pts',(-0.939820892206868,-3.33696855340067,
10.3841308342941));
#9534=CARTESIAN_POINT('Ctrl Pts',(2.2703379196763,-2.61992335659027,10.5414661499653));
#9535=CARTESIAN_POINT('Ctrl Pts',(3.43675322554079,0.455595550491001,10.6988014656364));
#9536=CARTESIAN_POINT('Ctrl Pts',(1.50917870869019,3.12106661837885,10.8561367813075));
#9537=CARTESIAN_POINT('Ctrl Pts',(-1.77673321502363,2.97670108175376,11.0134720969786));
#9538=CARTESIAN_POINT('Ctrl Pts',(-3.46368867729937,0.152965991767152,11.1708074126498));
#9539=CARTESIAN_POINT('Ctrl Pts',(-2.03158068936315,-2.80910804391069,11.3281427283209));
#9540=CARTESIAN_POINT('Ctrl Pts',(1.22756217529158,-3.24113439556783,11.485478043992));
#9541=CARTESIAN_POINT('Ctrl Pts',(3.38518042007578,-0.757767502188211,11.6428133596631));
#9542=CARTESIAN_POINT('Ctrl Pts',(2.48830916787281,2.41253151546626,11.8001486753343));
#9543=CARTESIAN_POINT('Ctrl Pts',(0.407565802433691,3.07068338225952,11.9050388857817));
#9544=CARTESIAN_POINT('Ctrl Pts',(-0.545102916878434,2.89105980740811,11.9574839910054));
#9545=CARTESIAN_POINT('Ctrl Pts',(-2.93989309841074,-0.00232834448912937,
10.1778238829104));
#9546=CARTESIAN_POINT('Ctrl Pts',(-2.94219554736775,-0.304542880453153,
10.1941477614813));
#9547=CARTESIAN_POINT('Ctrl Pts',(-2.89923296915434,-0.606119063222061,
10.2104716400522));
#9548=CARTESIAN_POINT('Ctrl Pts',(-2.80824451487588,-0.892433444227729,
10.226795518623));
#9549=CARTESIAN_POINT('Ctrl Pts',(-2.5159182127622,-1.81229987019432,10.2792406238467));
#9550=CARTESIAN_POINT('Ctrl Pts',(-1.72786955248453,-2.5746342117975,10.3316857290704));
#9551=CARTESIAN_POINT('Ctrl Pts',(-0.798818753698492,-2.83629384979735,
10.3841308342941));
#9552=CARTESIAN_POINT('Ctrl Pts',(0.130232045087536,-3.0979534877972,10.4365759395179));
#9553=CARTESIAN_POINT('Ctrl Pts',(1.20028498238192,-2.85893842219374,10.4890210447416));
#9554=CARTESIAN_POINT('Ctrl Pts',(1.92971400200653,-2.22684440487846,10.5414661499653));
#9555=CARTESIAN_POINT('Ctrl Pts',(2.65914302163113,-1.59475038756318,10.593911255189));
#9556=CARTESIAN_POINT('Ctrl Pts',(3.04794812358597,-0.569577418536059,10.6463563604127));
#9557=CARTESIAN_POINT('Ctrl Pts',(2.92108825508827,0.387254243958792,10.6988014656364));
#9558=CARTESIAN_POINT('Ctrl Pts',(2.79422838659058,1.34408590645364,10.7512465708601));
#9559=CARTESIAN_POINT('Ctrl Pts',(2.15170354764038,2.23257626241624,10.8036916760838));
#9560=CARTESIAN_POINT('Ctrl Pts',(1.28278914087964,2.6527605176267,10.8561367813075));
#9561=CARTESIAN_POINT('Ctrl Pts',(0.413874734118906,3.07294477283715,10.9085818865312));
#9562=CARTESIAN_POINT('Ctrl Pts',(-0.681429240452357,3.02482292729546,10.9610269917549));
#9563=CARTESIAN_POINT('Ctrl Pts',(-1.51024047145062,2.53013948952684,11.0134720969786));
#9564=CARTESIAN_POINT('Ctrl Pts',(-1.74480463118476,2.39013776105746,11.0283147313191));
#9565=CARTESIAN_POINT('Ctrl Pts',(-1.95802372783935,2.21436813426865,11.0431573656595));
#9566=CARTESIAN_POINT('Ctrl Pts',(-2.14415473270596,2.01243073062332,11.058));
#9567=CARTESIAN_POINT('Ctrl Pts',(-1.37989654081095,-1.933266887693,1.56125112837913E-17));
#9568=CARTESIAN_POINT('Ctrl Pts',(-1.44414345926609,-1.89839188587405,5.80920822621902E-18));
#9569=CARTESIAN_POINT('Ctrl Pts',(-1.5065284577229,-1.86047032724736,-1.41833741640826E-16));
#9570=CARTESIAN_POINT('Ctrl Pts',(-1.56680444439783,-1.81955553349441,-1.49186218934005E-16));
#9571=CARTESIAN_POINT('Ctrl Pts',(-1.63448180748404,-1.77361675247786,-1.62745475426733E-16));
#9572=CARTESIAN_POINT('Ctrl Pts',(-1.69950176926845,-1.72390575990714,4.47554715783556E-16));
#9573=CARTESIAN_POINT('Ctrl Pts',(-1.76178079551988,-1.6707784873017,5.27355936696949E-16));
#9574=CARTESIAN_POINT('Ctrl Pts',(-1.80277525259689,-1.63580806744237,5.79884178102324E-16));
#9575=CARTESIAN_POINT('Ctrl Pts',(-1.84258178887229,-1.59935636303953,9.13682232518509E-17));
#9576=CARTESIAN_POINT('Ctrl Pts',(-1.88117141744704,-1.56151405921777,1.59594559789866E-16));
#9577=CARTESIAN_POINT('Ctrl Pts',(-1.89157558896771,-1.55131137434519,1.77989100856589E-16));
#9578=CARTESIAN_POINT('Ctrl Pts',(-1.90188938652621,-1.54100934347453,3.40635361961997E-16));
#9579=CARTESIAN_POINT('Ctrl Pts',(-1.91210630257196,-1.53061605927472,3.05311331771918E-16));
#9580=CARTESIAN_POINT('Ctrl Pts',(-1.9724409846318,-1.46923985779222,9.67098202152561E-17));
#9581=CARTESIAN_POINT('Ctrl Pts',(-2.02946085491381,-1.40462521591101,1.4935214824922E-16));
#9582=CARTESIAN_POINT('Ctrl Pts',(-2.08307562783518,-1.33717477526203,1.38777878078145E-16));
#9583=CARTESIAN_POINT('Ctrl Pts',(-2.12998855414138,-1.27815563969417,1.29525391678454E-16));
#9584=CARTESIAN_POINT('Ctrl Pts',(-2.17429437900105,-1.21696417926775,2.01441503266146E-16));
#9585=CARTESIAN_POINT('Ctrl Pts',(-2.21591583956505,-1.15384057343859,1.52655665885959E-16));
#9586=CARTESIAN_POINT('Ctrl Pts',(-2.23664963326987,-1.12239545345888,1.28352927004359E-16));
#9587=CARTESIAN_POINT('Ctrl Pts',(-2.25671701785544,-1.09047047206691,-2.37280165770185E-16));
#9588=CARTESIAN_POINT('Ctrl Pts',(-2.2761066605572,-1.05809323638609,-2.63677968348475E-16));
#9589=CARTESIAN_POINT('Ctrl Pts',(-2.28578146762193,-1.0419380388242,-2.76849621421526E-16));
#9590=CARTESIAN_POINT('Ctrl Pts',(-2.29528887628369,-1.02566760843717,-1.10809144900277E-17));
#9591=CARTESIAN_POINT('Ctrl Pts',(-2.30461525834334,-1.0093071858719,0.));
#9592=CARTESIAN_POINT('Ctrl Pts',(-2.34846766322256,-0.932380906234359,
5.21021705459412E-17));
#9593=CARTESIAN_POINT('Ctrl Pts',(-2.38837887518559,-0.853373340579809,
-1.59588577561705E-17));
#9594=CARTESIAN_POINT('Ctrl Pts',(-2.42425706703596,-0.772682188207588,
-2.77555756156289E-17));
#9595=CARTESIAN_POINT('Ctrl Pts',(-2.46075963346513,-0.690586798283878,
-3.97575872863117E-17));
#9596=CARTESIAN_POINT('Ctrl Pts',(-2.49308822244858,-0.606748001409621,
2.24945356107799E-18));
#9597=CARTESIAN_POINT('Ctrl Pts',(-2.52111243497218,-0.521542915861604,
-2.77555756156289E-17));
#9598=CARTESIAN_POINT('Ctrl Pts',(-2.54406484395513,-0.4517581906252,-5.23303143573299E-17));
#9599=CARTESIAN_POINT('Ctrl Pts',(-2.56412941494483,-0.381055975787894,
-5.2234519399031E-17));
#9600=CARTESIAN_POINT('Ctrl Pts',(-2.58121358727312,-0.309628512371508,
-5.55111512312578E-17));
#9601=CARTESIAN_POINT('Ctrl Pts',(-2.59402671651933,-0.256057914809218,
-5.79686251054279E-17));
#9602=CARTESIAN_POINT('Ctrl Pts',(-2.6051630020304,-0.202079063721199,-1.68485553630616E-16));
#9603=CARTESIAN_POINT('Ctrl Pts',(-2.61457527537642,-0.147769877191515,
-1.94289029309402E-16));
#9604=CARTESIAN_POINT('Ctrl Pts',(-2.617136534184,-0.132991313371873,-2.01310646395843E-16));
#9605=CARTESIAN_POINT('Ctrl Pts',(-2.6195700893165,-0.118188277474481,-3.31395093795537E-16));
#9606=CARTESIAN_POINT('Ctrl Pts',(-2.6218748923051,-0.103362317982878,-3.33066907387547E-16));
#9607=CARTESIAN_POINT('Ctrl Pts',(-2.62397146608191,-0.089875821288789,
-3.34587679685255E-16));
#9608=CARTESIAN_POINT('Ctrl Pts',(-2.62596008221826,-0.076379405564125,
-2.78772373994456E-16));
#9609=CARTESIAN_POINT('Ctrl Pts',(-2.62784009463941,-0.0628763941457686,
-2.77555756156289E-16));
#9610=CARTESIAN_POINT('Ctrl Pts',(-2.64060982150785,0.0288409614284714,
-2.69292046128659E-16));
#9611=CARTESIAN_POINT('Ctrl Pts',(-2.64837710873961,0.12089024959815,-1.76997536955934E-16));
#9612=CARTESIAN_POINT('Ctrl Pts',(-2.65101366112809,0.212875307143708,-1.38777878078145E-16));
#9613=CARTESIAN_POINT('Ctrl Pts',(-2.65226659852151,0.256588270610049,-1.20615204739669E-16));
#9614=CARTESIAN_POINT('Ctrl Pts',(-2.65236023741492,0.300287183221066,-4.34987190636111E-16));
#9615=CARTESIAN_POINT('Ctrl Pts',(-2.6512772014093,0.343931535522003,-4.16333634234434E-16));
#9616=CARTESIAN_POINT('Ctrl Pts',(-2.64907421925761,0.432707650667494,-4.32903459206313E-16));
#9617=CARTESIAN_POINT('Ctrl Pts',(-2.64200629387468,0.521257644934972,-8.62622134822235E-17));
#9618=CARTESIAN_POINT('Ctrl Pts',(-2.63031624428264,0.609320814221094,-8.32667268468867E-17));
#9619=CARTESIAN_POINT('Ctrl Pts',(-2.61839797794639,0.699103179787949,-8.02127613999854E-17));
#9620=CARTESIAN_POINT('Ctrl Pts',(-2.60167524897612,0.788380265268053,1.49019320792917E-16));
#9621=CARTESIAN_POINT('Ctrl Pts',(-2.58035146554209,0.876878238745711,2.4980018054066E-16));
#9622=CARTESIAN_POINT('Ctrl Pts',(-2.57698234718955,0.890860754912604,2.65723370025807E-16));
#9623=CARTESIAN_POINT('Ctrl Pts',(-2.57349826551832,0.904823813068977,1.71128026421916E-16));
#9624=CARTESIAN_POINT('Ctrl Pts',(-2.56989990586492,0.918766319054272,1.94289029309402E-16));
#9625=CARTESIAN_POINT('Ctrl Pts',(-2.56629916621592,0.932718046770052,2.17465351145046E-16));
#9626=CARTESIAN_POINT('Ctrl Pts',(-2.56258611805641,0.946640891227604,-7.03868084514403E-16));
#9627=CARTESIAN_POINT('Ctrl Pts',(-2.55876298044222,0.960529869852388,-6.93889390390723E-16));
#9628=CARTESIAN_POINT('Ctrl Pts',(-2.53419843880054,1.04976976342104,-6.29773977327716E-16));
#9629=CARTESIAN_POINT('Ctrl Pts',(-2.50508011125346,1.13766264916498,6.87890529294335E-17));
#9630=CARTESIAN_POINT('Ctrl Pts',(-2.47169823504828,1.22392740477737,8.32667268468867E-17));
#9631=CARTESIAN_POINT('Ctrl Pts',(-2.43767482619284,1.31184999582573,9.80226325947151E-17));
#9632=CARTESIAN_POINT('Ctrl Pts',(-2.39922225163329,1.39808205966622,-2.50151931196036E-16));
#9633=CARTESIAN_POINT('Ctrl Pts',(-2.35659236008881,1.48232869936419,-2.77555756156289E-16));
#9634=CARTESIAN_POINT('Ctrl Pts',(-2.31360056696885,1.56729054124849,-3.05192222745878E-16));
#9635=CARTESIAN_POINT('Ctrl Pts',(-2.26635993703635,1.65023397727082,5.65740922539343E-17));
#9636=CARTESIAN_POINT('Ctrl Pts',(-2.21507658716517,1.73084671943837,5.55111512312578E-17));
#9637=CARTESIAN_POINT('Ctrl Pts',(-2.18435464293681,1.77913880985734,5.48743828668913E-17));
#9638=CARTESIAN_POINT('Ctrl Pts',(-2.15218088295609,1.82659422289983,-3.64380860772878E-16));
#9639=CARTESIAN_POINT('Ctrl Pts',(-2.11859145320912,1.87314213253736,-3.88578058618805E-16));
#9640=CARTESIAN_POINT('Ctrl Pts',(-2.10923966749503,1.88610174750099,-3.95314910385597E-16));
#9641=CARTESIAN_POINT('Ctrl Pts',(-2.09977706809611,1.89899226435558,-9.16981750261902E-17));
#9642=CARTESIAN_POINT('Ctrl Pts',(-2.0902160744712,1.91179680016256,-1.11022302462516E-16));
#9643=CARTESIAN_POINT('Ctrl Pts',(-2.03140899114824,1.99055403331781,-2.29879778669894E-16));
#9644=CARTESIAN_POINT('Ctrl Pts',(-1.96879105165951,2.06618994280669,4.68887291460301E-17));
#9645=CARTESIAN_POINT('Ctrl Pts',(-1.90263522085423,2.13839704217079,0.));
#9646=CARTESIAN_POINT('Ctrl Pts',(-1.83630675569242,2.21079256674222,-4.70110857922477E-17));
#9647=CARTESIAN_POINT('Ctrl Pts',(-1.76642150904269,2.27974226115238,-1.93865480317173E-16));
#9648=CARTESIAN_POINT('Ctrl Pts',(-1.6932045763485,2.34492041918897,-1.66533453693773E-16));
#9649=CARTESIAN_POINT('Ctrl Pts',(-1.62138195170811,2.40885735573024,-1.39721925040515E-16));
#9650=CARTESIAN_POINT('Ctrl Pts',(-1.54635279514513,2.46916580377976,-2.38947154895597E-16));
#9651=CARTESIAN_POINT('Ctrl Pts',(-1.46828869930752,2.52551090354043,-2.77555756156289E-16));
#9652=CARTESIAN_POINT('Ctrl Pts',(-1.41016377964657,2.56746430557163,-3.06302926317174E-16));
#9653=CARTESIAN_POINT('Ctrl Pts',(-1.35035542782446,2.60721994910279,8.78385754915914E-18));
#9654=CARTESIAN_POINT('Ctrl Pts',(-1.28892185405322,2.64462557919718,0.));
#9655=CARTESIAN_POINT('Origin',(0.,0.,0.));
#9656=CARTESIAN_POINT('Origin',(-1.44337567297407,-2.5,-6.));
#9657=CARTESIAN_POINT('',(-1.44337567297407,-2.5,-6.));
#9658=CARTESIAN_POINT('',(1.44337567297406,-2.5,-6.));
#9659=CARTESIAN_POINT('',(-0.721687836487033,-2.5,-6.));
#9660=CARTESIAN_POINT('',(-1.44337567297407,-2.5,-3.));
#9661=CARTESIAN_POINT('',(-1.44337567297407,-2.5,-6.));
#9662=CARTESIAN_POINT('',(1.44337567297406,-2.5,-3.));
#9663=CARTESIAN_POINT('',(-1.44337567297407,-2.5,-3.));
#9664=CARTESIAN_POINT('',(1.44337567297406,-2.5,-6.));
#9665=CARTESIAN_POINT('Origin',(-2.88675134594813,3.53525079574969E-16,
-6.));
#9666=CARTESIAN_POINT('',(-2.88675134594813,3.53525079574969E-16,-6.));
#9667=CARTESIAN_POINT('',(-2.52590742770461,-0.625,-6.));
#9668=CARTESIAN_POINT('',(-2.88675134594813,5.55111512312578E-16,-3.));
#9669=CARTESIAN_POINT('',(-2.88675134594813,3.53525079574969E-16,-6.));
#9670=CARTESIAN_POINT('',(-2.88675134594813,3.53525079574969E-16,-3.));
#9671=CARTESIAN_POINT('Origin',(-1.44337567297406,2.5,-6.));
#9672=CARTESIAN_POINT('',(-1.44337567297406,2.5,-6.));
#9673=CARTESIAN_POINT('',(-1.80421959121758,1.875,-6.));
#9674=CARTESIAN_POINT('',(-1.44337567297406,2.5,-3.));
#9675=CARTESIAN_POINT('',(-1.44337567297406,2.5,-6.));
#9676=CARTESIAN_POINT('',(-1.44337567297406,2.5,-3.));
#9677=CARTESIAN_POINT('Origin',(1.44337567297406,2.5,-6.));
#9678=CARTESIAN_POINT('',(1.44337567297406,2.5,-6.));
#9679=CARTESIAN_POINT('',(0.721687836487033,2.5,-6.));
#9680=CARTESIAN_POINT('',(1.44337567297406,2.5,-3.));
#9681=CARTESIAN_POINT('',(1.44337567297406,2.5,-6.));
#9682=CARTESIAN_POINT('',(1.44337567297406,2.5,-3.));
#9683=CARTESIAN_POINT('Origin',(2.88675134594813,0.,-6.));
#9684=CARTESIAN_POINT('',(2.88675134594813,0.,-6.));
#9685=CARTESIAN_POINT('',(2.52590742770461,0.625,-6.));
#9686=CARTESIAN_POINT('',(2.88675134594813,0.,-3.));
#9687=CARTESIAN_POINT('',(2.88675134594813,0.,-6.));
#9688=CARTESIAN_POINT('',(2.88675134594813,0.,-3.));
#9689=CARTESIAN_POINT('Origin',(1.44337567297406,-2.5,-6.));
#9690=CARTESIAN_POINT('',(1.80421959121758,-1.875,-6.));
#9691=CARTESIAN_POINT('',(1.44337567297406,-2.5,-3.));
#9692=CARTESIAN_POINT('Origin',(0.,0.,-3.));
#9693=CARTESIAN_POINT('Origin',(0.,0.,0.));
#9694=CARTESIAN_POINT('',(-5.,-6.12323399573677E-16,0.));
#9695=CARTESIAN_POINT('Origin',(0.,0.,0.));
#9696=CARTESIAN_POINT('Origin',(0.,0.,-6.));
#9697=CARTESIAN_POINT('',(-5.,-6.12323399573677E-16,-6.));
#9698=CARTESIAN_POINT('',(-5.,-6.12323399573677E-16,-6.));
#9699=CARTESIAN_POINT('Origin',(0.,0.,-6.));
#9700=CARTESIAN_POINT('Origin',(0.,0.,-6.));
#9701=CARTESIAN_POINT('Origin',(0.,0.,12.));
#9763=UNCERTAINTY_MEASURE_WITH_UNIT(LENGTH_MEASURE(0.01),#9778,
'DISTANCE_ACCURACY_VALUE',
'Maximum model space distance between geometric entities at asserted c
onnectivities');
#9764=UNCERTAINTY_MEASURE_WITH_UNIT(LENGTH_MEASURE(0.01),#9778,
'DISTANCE_ACCURACY_VALUE',
'Maximum model space distance between geometric entities at asserted c
onnectivities');
#9776=(
GEOMETRIC_REPRESENTATION_CONTEXT(3)
GLOBAL_UNCERTAINTY_ASSIGNED_CONTEXT((#9763))
GLOBAL_UNIT_ASSIGNED_CONTEXT((#9778,#9780,#9781))
REPRESENTATION_CONTEXT('','3D')
);
#9777=(
GEOMETRIC_REPRESENTATION_CONTEXT(3)
GLOBAL_UNCERTAINTY_ASSIGNED_CONTEXT((#9764))
GLOBAL_UNIT_ASSIGNED_CONTEXT((#9778,#9780,#9781))
REPRESENTATION_CONTEXT('','3D')
);
#9778=(
LENGTH_UNIT()
NAMED_UNIT(*)
SI_UNIT(.MILLI.,.METRE.)
);
#9780=(
NAMED_UNIT(*)
PLANE_ANGLE_UNIT()
SI_UNIT($,.RADIAN.)
);
#9781=(
NAMED_UNIT(*)
SI_UNIT($,.STERADIAN.)
SOLID_ANGLE_UNIT()
);
#9793=SHAPE_DEFINITION_REPRESENTATION(#9805,#9867);
#9805=PRODUCT_DEFINITION_SHAPE('',$,#9880);
#9867=SHAPE_REPRESENTATION('',(#4258),#9776);
#9868=PRODUCT_DEFINITION_CONTEXT('part definition',#9906,'design');
#9880=PRODUCT_DEFINITION('Socket head cap screw M6x12',
'Socket head cap screw M6x12',#9892,#9868);
#9892=PRODUCT_DEFINITION_FORMATION('',$,#9919);
#9906=APPLICATION_CONTEXT(
'Core Data for Automotive Mechanical Design Process');
#9907=PRODUCT_CONTEXT('part definition',#9906,'mechanical');
#9919=PRODUCT('Socket head cap screw M6x12',
'Socket head cap screw M6x12',$,(#9907));
#9930=PRESENTATION_STYLE_ASSIGNMENT((#9941));
#9941=SURFACE_STYLE_USAGE(.BOTH.,#9952);
#9952=SURFACE_SIDE_STYLE('',(#9963));
#9963=SURFACE_STYLE_FILL_AREA(#9974);
#9974=FILL_AREA_STYLE('Dark gray',(#9985));
#9985=FILL_AREA_STYLE_COLOUR('Dark gray',#9996);
#9996=COLOUR_RGB('Dark gray',0.250980392156863,0.282352941176471,0.32156862745098);
ENDSEC;
END-ISO-10303-21;
